ISO-10303-21;
HEADER;
/* Generated by software containing ST-Developer
 * from STEP Tools, Inc. (www.steptools.com) 
 */

FILE_DESCRIPTION(
/* description */ (''),
/* implementation_level */ '2;1');

FILE_NAME(
/* name */ 
'05_Adjustable_Mirror_Plate_56x56.step',
/* time_stamp */ '2026-10-20T10:06:23-07:00',
/* author */ (''),
/* organization */ (''),
/* preprocessor_version */ 'ST-DEVELOPER v20.2',
/* originating_system */ 'Autodesk Translation Framework v15.15.0.0',
/* authorisation */ '');

FILE_SCHEMA (('AUTOMOTIVE_DESIGN { 1 0 10303 214 3 1 1 }'));
ENDSEC;

DATA;
#10=MECHANICAL_DESIGN_GEOMETRIC_PRESENTATION_REPRESENTATION('',(#463),#38611);
#435=SHAPE_REPRESENTATION_RELATIONSHIP('SRR','None',#38671,#449);
#449=ADVANCED_BREP_SHAPE_REPRESENTATION('',(#477),#38600);
#463=STYLED_ITEM('',(#38871),#477);
#477=MANIFOLD_SOLID_BREP('Mirror plate',#16237);
#896=CYLINDRICAL_SURFACE('',#16701,1.1);
#897=CYLINDRICAL_SURFACE('',#16716,1.26);
#898=CYLINDRICAL_SURFACE('',#16719,1.355);
#899=CYLINDRICAL_SURFACE('',#16722,0.225);
#900=CYLINDRICAL_SURFACE('',#16731,0.225000000000001);
#901=CYLINDRICAL_SURFACE('',#16740,0.255);
#902=CYLINDRICAL_SURFACE('',#16744,0.255000000000001);
#903=CYLINDRICAL_SURFACE('',#16748,0.255);
#904=CYLINDRICAL_SURFACE('',#16759,0.4);
#905=CYLINDRICAL_SURFACE('',#16762,0.4);
#1169=FACE_BOUND('',#2892,.T.);
#1170=FACE_BOUND('',#2893,.T.);
#1171=FACE_BOUND('',#2894,.T.);
#1172=FACE_BOUND('',#2895,.T.);
#1173=FACE_BOUND('',#2896,.T.);
#1174=FACE_BOUND('',#2897,.T.);
#1175=FACE_BOUND('',#2908,.T.);
#1176=FACE_BOUND('',#2911,.T.);
#1177=FACE_BOUND('',#2919,.T.);
#1178=FACE_BOUND('',#2924,.T.);
#1179=FACE_BOUND('',#2933,.T.);
#1180=FACE_BOUND('',#2934,.T.);
#1181=FACE_BOUND('',#2935,.T.);
#1182=FACE_BOUND('',#2936,.T.);
#1183=FACE_BOUND('',#2937,.T.);
#1184=FACE_BOUND('',#2938,.T.);
#1293=CIRCLE('',#16685,0.254999999999999);
#1294=CIRCLE('',#16686,0.285);
#1295=CIRCLE('',#16687,0.285);
#1296=CIRCLE('',#16688,0.285);
#1297=CIRCLE('',#16689,0.255000000000001);
#1298=CIRCLE('',#16690,1.385);
#1299=CIRCLE('',#16697,1.1);
#1300=CIRCLE('',#16698,1.1);
#1301=CIRCLE('',#16699,1.1212132034356);
#1302=CIRCLE('',#16700,1.1212132034356);
#1303=CIRCLE('',#16702,1.1);
#1304=CIRCLE('',#16703,1.1);
#1305=CIRCLE('',#16705,1.1287867965644);
#1306=CIRCLE('',#16707,1.13);
#1307=CIRCLE('',#16709,1.26);
#1308=CIRCLE('',#16711,1.29);
#1309=CIRCLE('',#16712,1.26);
#1310=CIRCLE('',#16713,1.26);
#1311=CIRCLE('',#16715,1.355);
#1312=CIRCLE('',#16718,1.355);
#1313=CIRCLE('',#16721,0.225);
#1314=CIRCLE('',#16723,0.225);
#1315=CIRCLE('',#16724,0.225);
#1316=CIRCLE('',#16726,0.254999999999999);
#1317=CIRCLE('',#16728,0.4);
#1318=CIRCLE('',#16730,0.225000000000001);
#1319=CIRCLE('',#16732,0.225000000000001);
#1320=CIRCLE('',#16733,0.225000000000001);
#1321=CIRCLE('',#16735,0.255000000000001);
#1322=CIRCLE('',#16737,0.4);
#1323=CIRCLE('',#16739,0.255);
#1324=CIRCLE('',#16741,0.255);
#1325=CIRCLE('',#16743,0.255000000000001);
#1326=CIRCLE('',#16745,0.255000000000001);
#1327=CIRCLE('',#16747,0.255);
#1328=CIRCLE('',#16749,0.255);
#1329=CIRCLE('',#16751,0.430000000000001);
#1330=CIRCLE('',#16752,0.4);
#1331=CIRCLE('',#16754,0.43);
#1332=CIRCLE('',#16755,0.285);
#1333=CIRCLE('',#16756,0.285);
#1334=CIRCLE('',#16757,0.285);
#1335=CIRCLE('',#16758,1.18);
#1336=CIRCLE('',#16761,0.4);
#1715=CONICAL_SURFACE('',#16696,1.1106066017178,0.392699081698722);
#1716=CONICAL_SURFACE('',#16704,1.14,0.785398163397448);
#1717=CONICAL_SURFACE('',#16706,1.115,0.785398163397448);
#1718=CONICAL_SURFACE('',#16710,1.275,0.785398163397448);
#1719=CONICAL_SURFACE('',#16717,1.37,0.785398163397449);
#1720=CONICAL_SURFACE('',#16720,0.239999999999999,0.785398163397438);
#1721=CONICAL_SURFACE('',#16725,0.239999999999999,0.785398163397438);
#1722=CONICAL_SURFACE('',#16729,0.240000000000001,0.785398163397452);
#1723=CONICAL_SURFACE('',#16734,0.240000000000001,0.785398163397452);
#1724=CONICAL_SURFACE('',#16738,0.27,0.785398163397452);
#1725=CONICAL_SURFACE('',#16742,0.27,0.785398163397437);
#1726=CONICAL_SURFACE('',#16746,0.27,0.785398163397452);
#1727=CONICAL_SURFACE('',#16750,0.415,0.785398163397452);
#1728=CONICAL_SURFACE('',#16760,0.415,0.785398163397437);
#1729=CONICAL_SURFACE('',#16763,1.1543933982822,1.17809724509617);
#1730=CONICAL_SURFACE('',#16768,0.27,0.785398163397452);
#1731=CONICAL_SURFACE('',#16769,0.27,0.785398163397437);
#1732=CONICAL_SURFACE('',#16770,0.27,0.785398163397452);
#1930=FACE_OUTER_BOUND('',#2857,.T.);
#1931=FACE_OUTER_BOUND('',#2858,.T.);
#1932=FACE_OUTER_BOUND('',#2859,.T.);
#1933=FACE_OUTER_BOUND('',#2860,.T.);
#1934=FACE_OUTER_BOUND('',#2861,.T.);
#1935=FACE_OUTER_BOUND('',#2862,.T.);
#1936=FACE_OUTER_BOUND('',#2863,.T.);
#1937=FACE_OUTER_BOUND('',#2864,.T.);
#1938=FACE_OUTER_BOUND('',#2865,.T.);
#1939=FACE_OUTER_BOUND('',#2866,.T.);
#1940=FACE_OUTER_BOUND('',#2867,.T.);
#1941=FACE_OUTER_BOUND('',#2868,.T.);
#1942=FACE_OUTER_BOUND('',#2869,.T.);
#1943=FACE_OUTER_BOUND('',#2870,.T.);
#1944=FACE_OUTER_BOUND('',#2871,.T.);
#1945=FACE_OUTER_BOUND('',#2872,.T.);
#1946=FACE_OUTER_BOUND('',#2873,.T.);
#1947=FACE_OUTER_BOUND('',#2874,.T.);
#1948=FACE_OUTER_BOUND('',#2875,.T.);
#1949=FACE_OUTER_BOUND('',#2876,.T.);
#1950=FACE_OUTER_BOUND('',#2877,.T.);
#1951=FACE_OUTER_BOUND('',#2878,.T.);
#1952=FACE_OUTER_BOUND('',#2879,.T.);
#1953=FACE_OUTER_BOUND('',#2880,.T.);
#1954=FACE_OUTER_BOUND('',#2881,.T.);
#1955=FACE_OUTER_BOUND('',#2882,.T.);
#1956=FACE_OUTER_BOUND('',#2883,.T.);
#1957=FACE_OUTER_BOUND('',#2884,.T.);
#1958=FACE_OUTER_BOUND('',#2885,.T.);
#1959=FACE_OUTER_BOUND('',#2886,.T.);
#1960=FACE_OUTER_BOUND('',#2887,.T.);
#1961=FACE_OUTER_BOUND('',#2888,.T.);
#1962=FACE_OUTER_BOUND('',#2889,.T.);
#1963=FACE_OUTER_BOUND('',#2890,.T.);
#1964=FACE_OUTER_BOUND('',#2891,.T.);
#1965=FACE_OUTER_BOUND('',#2898,.T.);
#1966=FACE_OUTER_BOUND('',#2899,.T.);
#1967=FACE_OUTER_BOUND('',#2900,.T.);
#1968=FACE_OUTER_BOUND('',#2901,.T.);
#1969=FACE_OUTER_BOUND('',#2902,.T.);
#1970=FACE_OUTER_BOUND('',#2903,.T.);
#1971=FACE_OUTER_BOUND('',#2904,.T.);
#1972=FACE_OUTER_BOUND('',#2905,.T.);
#1973=FACE_OUTER_BOUND('',#2906,.T.);
#1974=FACE_OUTER_BOUND('',#2907,.T.);
#1975=FACE_OUTER_BOUND('',#2909,.T.);
#1976=FACE_OUTER_BOUND('',#2910,.T.);
#1977=FACE_OUTER_BOUND('',#2912,.T.);
#1978=FACE_OUTER_BOUND('',#2913,.T.);
#1979=FACE_OUTER_BOUND('',#2914,.T.);
#1980=FACE_OUTER_BOUND('',#2915,.T.);
#1981=FACE_OUTER_BOUND('',#2916,.T.);
#1982=FACE_OUTER_BOUND('',#2917,.T.);
#1983=FACE_OUTER_BOUND('',#2918,.T.);
#1984=FACE_OUTER_BOUND('',#2920,.T.);
#1985=FACE_OUTER_BOUND('',#2921,.T.);
#1986=FACE_OUTER_BOUND('',#2922,.T.);
#1987=FACE_OUTER_BOUND('',#2923,.T.);
#1988=FACE_OUTER_BOUND('',#2925,.T.);
#1989=FACE_OUTER_BOUND('',#2926,.T.);
#1990=FACE_OUTER_BOUND('',#2927,.T.);
#1991=FACE_OUTER_BOUND('',#2928,.T.);
#1992=FACE_OUTER_BOUND('',#2929,.T.);
#1993=FACE_OUTER_BOUND('',#2930,.T.);
#1994=FACE_OUTER_BOUND('',#2931,.T.);
#1995=FACE_OUTER_BOUND('',#2932,.T.);
#1996=FACE_OUTER_BOUND('',#2939,.T.);
#1997=FACE_OUTER_BOUND('',#2940,.T.);
#1998=FACE_OUTER_BOUND('',#2941,.T.);
#1999=FACE_OUTER_BOUND('',#2942,.T.);
#2000=FACE_OUTER_BOUND('',#2943,.T.);
#2001=FACE_OUTER_BOUND('',#2944,.T.);
#2002=FACE_OUTER_BOUND('',#2945,.T.);
#2003=FACE_OUTER_BOUND('',#2946,.T.);
#2004=FACE_OUTER_BOUND('',#2947,.T.);
#2005=FACE_OUTER_BOUND('',#2948,.T.);
#2006=FACE_OUTER_BOUND('',#2949,.T.);
#2007=FACE_OUTER_BOUND('',#2950,.T.);
#2008=FACE_OUTER_BOUND('',#2951,.T.);
#2009=FACE_OUTER_BOUND('',#2952,.T.);
#2857=EDGE_LOOP('',(#10753,#10754,#10755,#10756,#10757,#10758));
#2858=EDGE_LOOP('',(#10759,#10760,#10761,#10762,#10763,#10764));
#2859=EDGE_LOOP('',(#10765,#10766,#10767,#10768,#10769,#10770,#10771,#10772,
#10773));
#2860=EDGE_LOOP('',(#10774,#10775,#10776,#10777));
#2861=EDGE_LOOP('',(#10778,#10779,#10780,#10781,#10782,#10783));
#2862=EDGE_LOOP('',(#10784,#10785,#10786,#10787));
#2863=EDGE_LOOP('',(#10788,#10789,#10790,#10791,#10792,#10793,#10794,#10795,
#10796));
#2864=EDGE_LOOP('',(#10797,#10798,#10799,#10800,#10801,#10802));
#2865=EDGE_LOOP('',(#10803,#10804,#10805,#10806,#10807,#10808,#10809,#10810));
#2866=EDGE_LOOP('',(#10811,#10812,#10813,#10814,#10815,#10816));
#2867=EDGE_LOOP('',(#10817,#10818,#10819,#10820,#10821,#10822));
#2868=EDGE_LOOP('',(#10823,#10824,#10825,#10826));
#2869=EDGE_LOOP('',(#10827,#10828,#10829,#10830,#10831,#10832));
#2870=EDGE_LOOP('',(#10833,#10834,#10835,#10836));
#2871=EDGE_LOOP('',(#10837,#10838,#10839,#10840,#10841,#10842,#10843,#10844,
#10845));
#2872=EDGE_LOOP('',(#10846,#10847,#10848,#10849,#10850,#10851));
#2873=EDGE_LOOP('',(#10852,#10853,#10854,#10855,#10856,#10857));
#2874=EDGE_LOOP('',(#10858,#10859,#10860,#10861));
#2875=EDGE_LOOP('',(#10862,#10863,#10864,#10865,#10866,#10867));
#2876=EDGE_LOOP('',(#10868,#10869,#10870,#10871,#10872,#10873));
#2877=EDGE_LOOP('',(#10874,#10875,#10876,#10877,#10878,#10879,#10880,#10881));
#2878=EDGE_LOOP('',(#10882,#10883,#10884,#10885,#10886,#10887,#10888,#10889,
#10890));
#2879=EDGE_LOOP('',(#10891,#10892,#10893,#10894));
#2880=EDGE_LOOP('',(#10895,#10896,#10897,#10898,#10899,#10900,#10901,#10902));
#2881=EDGE_LOOP('',(#10903,#10904,#10905,#10906,#10907,#10908));
#2882=EDGE_LOOP('',(#10909,#10910,#10911,#10912,#10913,#10914));
#2883=EDGE_LOOP('',(#10915,#10916,#10917,#10918));
#2884=EDGE_LOOP('',(#10919,#10920,#10921,#10922,#10923,#10924));
#2885=EDGE_LOOP('',(#10925,#10926,#10927,#10928,#10929,#10930));
#2886=EDGE_LOOP('',(#10931,#10932,#10933,#10934));
#2887=EDGE_LOOP('',(#10935,#10936,#10937,#10938,#10939,#10940));
#2888=EDGE_LOOP('',(#10941,#10942,#10943,#10944,#10945,#10946));
#2889=EDGE_LOOP('',(#10947,#10948,#10949,#10950));
#2890=EDGE_LOOP('',(#10951,#10952,#10953,#10954,#10955,#10956));
#2891=EDGE_LOOP('',(#10957,#10958,#10959,#10960));
#2892=EDGE_LOOP('',(#10961));
#2893=EDGE_LOOP('',(#10962));
#2894=EDGE_LOOP('',(#10963));
#2895=EDGE_LOOP('',(#10964));
#2896=EDGE_LOOP('',(#10965));
#2897=EDGE_LOOP('',(#10966));
#2898=EDGE_LOOP('',(#10967,#10968,#10969,#10970,#10971,#10972));
#2899=EDGE_LOOP('',(#10973,#10974,#10975,#10976));
#2900=EDGE_LOOP('',(#10977,#10978,#10979,#10980,#10981,#10982));
#2901=EDGE_LOOP('',(#10983,#10984,#10985,#10986));
#2902=EDGE_LOOP('',(#10987,#10988,#10989,#10990,#10991,#10992,#10993,#10994));
#2903=EDGE_LOOP('',(#10995,#10996,#10997,#10998,#10999,#11000));
#2904=EDGE_LOOP('',(#11001,#11002,#11003,#11004,#11005,#11006));
#2905=EDGE_LOOP('',(#11007,#11008,#11009,#11010,#11011));
#2906=EDGE_LOOP('',(#11012,#11013,#11014,#11015,#11016));
#2907=EDGE_LOOP('',(#11017));
#2908=EDGE_LOOP('',(#11018));
#2909=EDGE_LOOP('',(#11019,#11020,#11021,#11022,#11023));
#2910=EDGE_LOOP('',(#11024));
#2911=EDGE_LOOP('',(#11025));
#2912=EDGE_LOOP('',(#11026,#11027,#11028,#11029,#11030));
#2913=EDGE_LOOP('',(#11031,#11032,#11033,#11034));
#2914=EDGE_LOOP('',(#11035,#11036,#11037,#11038));
#2915=EDGE_LOOP('',(#11039,#11040,#11041,#11042));
#2916=EDGE_LOOP('',(#11043,#11044,#11045,#11046,#11047));
#2917=EDGE_LOOP('',(#11048,#11049,#11050,#11051,#11052));
#2918=EDGE_LOOP('',(#11053));
#2919=EDGE_LOOP('',(#11054));
#2920=EDGE_LOOP('',(#11055,#11056,#11057,#11058));
#2921=EDGE_LOOP('',(#11059,#11060,#11061,#11062,#11063));
#2922=EDGE_LOOP('',(#11064,#11065,#11066,#11067,#11068));
#2923=EDGE_LOOP('',(#11069));
#2924=EDGE_LOOP('',(#11070));
#2925=EDGE_LOOP('',(#11071,#11072,#11073,#11074));
#2926=EDGE_LOOP('',(#11075,#11076,#11077,#11078));
#2927=EDGE_LOOP('',(#11079,#11080,#11081,#11082));
#2928=EDGE_LOOP('',(#11083,#11084,#11085,#11086));
#2929=EDGE_LOOP('',(#11087,#11088,#11089,#11090));
#2930=EDGE_LOOP('',(#11091,#11092,#11093,#11094));
#2931=EDGE_LOOP('',(#11095,#11096,#11097,#11098));
#2932=EDGE_LOOP('',(#11099,#11100,#11101,#11102));
#2933=EDGE_LOOP('',(#11103));
#2934=EDGE_LOOP('',(#11104));
#2935=EDGE_LOOP('',(#11105));
#2936=EDGE_LOOP('',(#11106));
#2937=EDGE_LOOP('',(#11107));
#2938=EDGE_LOOP('',(#11108));
#2939=EDGE_LOOP('',(#11109,#11110,#11111,#11112));
#2940=EDGE_LOOP('',(#11113,#11114,#11115,#11116));
#2941=EDGE_LOOP('',(#11117,#11118,#11119,#11120));
#2942=EDGE_LOOP('',(#11121,#11122,#11123,#11124));
#2943=EDGE_LOOP('',(#11125,#11126,#11127,#11128,#11129,#11130));
#2944=EDGE_LOOP('',(#11131,#11132,#11133,#11134,#11135,#11136));
#2945=EDGE_LOOP('',(#11137,#11138,#11139,#11140,#11141,#11142));
#2946=EDGE_LOOP('',(#11143,#11144,#11145,#11146,#11147,#11148));
#2947=EDGE_LOOP('',(#11149,#11150,#11151,#11152));
#2948=EDGE_LOOP('',(#11153,#11154,#11155,#11156));
#2949=EDGE_LOOP('',(#11157,#11158,#11159,#11160));
#2950=EDGE_LOOP('',(#11161,#11162,#11163,#11164));
#2951=EDGE_LOOP('',(#11165,#11166,#11167,#11168));
#2952=EDGE_LOOP('',(#11169,#11170,#11171,#11172));
#3915=LINE('',#22965,#5139);
#3916=LINE('',#22967,#5140);
#3917=LINE('',#22969,#5141);
#3918=LINE('',#22971,#5142);
#3919=LINE('',#22973,#5143);
#3920=LINE('',#22974,#5144);
#3921=LINE('',#22977,#5145);
#3922=LINE('',#22979,#5146);
#3923=LINE('',#22981,#5147);
#3924=LINE('',#22983,#5148);
#3925=LINE('',#22984,#5149);
#3926=LINE('',#22987,#5150);
#3927=LINE('',#22989,#5151);
#3928=LINE('',#22991,#5152);
#3929=LINE('',#22993,#5153);
#3930=LINE('',#22995,#5154);
#3931=LINE('',#22997,#5155);
#3932=LINE('',#22998,#5156);
#3933=LINE('',#23001,#5157);
#3934=LINE('',#23002,#5158);
#3935=LINE('',#23005,#5159);
#3936=LINE('',#23007,#5160);
#3937=LINE('',#23009,#5161);
#3938=LINE('',#23011,#5162);
#3939=LINE('',#23012,#5163);
#3940=LINE('',#23014,#5164);
#3941=LINE('',#23017,#5165);
#3942=LINE('',#23019,#5166);
#3943=LINE('',#23021,#5167);
#3944=LINE('',#23023,#5168);
#3945=LINE('',#23025,#5169);
#3946=LINE('',#23026,#5170);
#3947=LINE('',#23029,#5171);
#3948=LINE('',#23031,#5172);
#3949=LINE('',#23032,#5173);
#3950=LINE('',#23035,#5174);
#3951=LINE('',#23037,#5175);
#3952=LINE('',#23039,#5176);
#3953=LINE('',#23041,#5177);
#3954=LINE('',#23043,#5178);
#3955=LINE('',#23044,#5179);
#3956=LINE('',#23048,#5180);
#3957=LINE('',#23049,#5181);
#3958=LINE('',#23051,#5182);
#3959=LINE('',#23053,#5183);
#3960=LINE('',#23054,#5184);
#3961=LINE('',#23057,#5185);
#3962=LINE('',#23059,#5186);
#3963=LINE('',#23061,#5187);
#3964=LINE('',#23063,#5188);
#3965=LINE('',#23064,#5189);
#3966=LINE('',#23067,#5190);
#3967=LINE('',#23068,#5191);
#3968=LINE('',#23071,#5192);
#3969=LINE('',#23073,#5193);
#3970=LINE('',#23074,#5194);
#3971=LINE('',#23077,#5195);
#3972=LINE('',#23078,#5196);
#3973=LINE('',#23081,#5197);
#3974=LINE('',#23083,#5198);
#3975=LINE('',#23085,#5199);
#3976=LINE('',#23087,#5200);
#3977=LINE('',#23089,#5201);
#3978=LINE('',#23090,#5202);
#3979=LINE('',#23094,#5203);
#3980=LINE('',#23095,#5204);
#3981=LINE('',#23097,#5205);
#3982=LINE('',#23099,#5206);
#3983=LINE('',#23100,#5207);
#3984=LINE('',#23103,#5208);
#3985=LINE('',#23105,#5209);
#3986=LINE('',#23107,#5210);
#3987=LINE('',#23109,#5211);
#3988=LINE('',#23110,#5212);
#3989=LINE('',#23113,#5213);
#3990=LINE('',#23114,#5214);
#3991=LINE('',#23117,#5215);
#3992=LINE('',#23119,#5216);
#3993=LINE('',#23120,#5217);
#3994=LINE('',#23123,#5218);
#3995=LINE('',#23125,#5219);
#3996=LINE('',#23126,#5220);
#3997=LINE('',#23129,#5221);
#3998=LINE('',#23131,#5222);
#3999=LINE('',#23133,#5223);
#4000=LINE('',#23134,#5224);
#4001=LINE('',#23135,#5225);
#4002=LINE('',#23138,#5226);
#4003=LINE('',#23140,#5227);
#4004=LINE('',#23142,#5228);
#4005=LINE('',#23144,#5229);
#4006=LINE('',#23146,#5230);
#4007=LINE('',#23148,#5231);
#4008=LINE('',#23149,#5232);
#4009=LINE('',#23152,#5233);
#4010=LINE('',#23153,#5234);
#4011=LINE('',#23156,#5235);
#4012=LINE('',#23158,#5236);
#4013=LINE('',#23160,#5237);
#4014=LINE('',#23162,#5238);
#4015=LINE('',#23163,#5239);
#4016=LINE('',#23165,#5240);
#4017=LINE('',#23167,#5241);
#4018=LINE('',#23169,#5242);
#4019=LINE('',#23170,#5243);
#4020=LINE('',#23173,#5244);
#4021=LINE('',#23174,#5245);
#4022=LINE('',#23176,#5246);
#4023=LINE('',#23179,#5247);
#4024=LINE('',#23180,#5248);
#4025=LINE('',#23181,#5249);
#4026=LINE('',#23183,#5250);
#4027=LINE('',#23184,#5251);
#4028=LINE('',#23187,#5252);
#4029=LINE('',#23189,#5253);
#4030=LINE('',#23191,#5254);
#4031=LINE('',#23192,#5255);
#4032=LINE('',#23195,#5256);
#4033=LINE('',#23196,#5257);
#4034=LINE('',#23200,#5258);
#4035=LINE('',#23201,#5259);
#4036=LINE('',#23203,#5260);
#4037=LINE('',#23218,#5261);
#4038=LINE('',#23221,#5262);
#4039=LINE('',#23222,#5263);
#4040=LINE('',#23225,#5264);
#4041=LINE('',#23226,#5265);
#4042=LINE('',#23229,#5266);
#4043=LINE('',#23230,#5267);
#4044=LINE('',#23231,#5268);
#4045=LINE('',#23238,#5269);
#4046=LINE('',#23247,#5270);
#4047=LINE('',#23250,#5271);
#4048=LINE('',#23255,#5272);
#4049=LINE('',#23263,#5273);
#4050=LINE('',#23271,#5274);
#4051=LINE('',#23274,#5275);
#4052=LINE('',#23277,#5276);
#4053=LINE('',#23280,#5277);
#4054=LINE('',#23287,#5278);
#4055=LINE('',#23291,#5279);
#4056=LINE('',#23297,#5280);
#4057=LINE('',#23304,#5281);
#4058=LINE('',#23308,#5282);
#4059=LINE('',#23314,#5283);
#4060=LINE('',#23319,#5284);
#4061=LINE('',#23322,#5285);
#4062=LINE('',#23327,#5286);
#4063=LINE('',#23330,#5287);
#4064=LINE('',#23335,#5288);
#4065=LINE('',#23340,#5289);
#4066=LINE('',#23345,#5290);
#4067=LINE('',#23347,#5291);
#4068=LINE('',#23349,#5292);
#4069=LINE('',#23350,#5293);
#4070=LINE('',#23362,#5294);
#4071=LINE('',#23365,#5295);
#4072=LINE('',#23368,#5296);
#4073=LINE('',#23370,#5297);
#4074=LINE('',#23372,#5298);
#4075=LINE('',#23373,#5299);
#4076=LINE('',#23375,#5300);
#4077=LINE('',#23377,#5301);
#4078=LINE('',#23380,#5302);
#4079=LINE('',#23382,#5303);
#4080=LINE('',#23384,#5304);
#5139=VECTOR('',#18562,1.);
#5140=VECTOR('',#18563,1.);
#5141=VECTOR('',#18564,1.);
#5142=VECTOR('',#18565,1.);
#5143=VECTOR('',#18566,1.);
#5144=VECTOR('',#18567,1.);
#5145=VECTOR('',#18570,1.);
#5146=VECTOR('',#18571,1.);
#5147=VECTOR('',#18572,1.);
#5148=VECTOR('',#18573,1.);
#5149=VECTOR('',#18574,1.);
#5150=VECTOR('',#18577,1.);
#5151=VECTOR('',#18578,1.);
#5152=VECTOR('',#18579,1.);
#5153=VECTOR('',#18580,1.);
#5154=VECTOR('',#18581,1.);
#5155=VECTOR('',#18582,1.);
#5156=VECTOR('',#18583,1.);
#5157=VECTOR('',#18586,1.);
#5158=VECTOR('',#18587,1.);
#5159=VECTOR('',#18590,1.);
#5160=VECTOR('',#18591,1.);
#5161=VECTOR('',#18592,1.);
#5162=VECTOR('',#18593,1.);
#5163=VECTOR('',#18594,1.);
#5164=VECTOR('',#18597,1.);
#5165=VECTOR('',#18600,1.);
#5166=VECTOR('',#18601,1.);
#5167=VECTOR('',#18602,1.);
#5168=VECTOR('',#18603,1.);
#5169=VECTOR('',#18604,1.);
#5170=VECTOR('',#18605,1.);
#5171=VECTOR('',#18608,1.);
#5172=VECTOR('',#18609,1.);
#5173=VECTOR('',#18610,1.);
#5174=VECTOR('',#18613,1.);
#5175=VECTOR('',#18614,1.);
#5176=VECTOR('',#18615,1.);
#5177=VECTOR('',#18616,1.);
#5178=VECTOR('',#18617,1.);
#5179=VECTOR('',#18618,1.);
#5180=VECTOR('',#18621,1.);
#5181=VECTOR('',#18622,1.);
#5182=VECTOR('',#18623,1.);
#5183=VECTOR('',#18624,1.);
#5184=VECTOR('',#18625,1.);
#5185=VECTOR('',#18628,1.);
#5186=VECTOR('',#18629,1.);
#5187=VECTOR('',#18630,1.);
#5188=VECTOR('',#18631,1.);
#5189=VECTOR('',#18632,1.);
#5190=VECTOR('',#18635,1.);
#5191=VECTOR('',#18636,1.);
#5192=VECTOR('',#18639,1.);
#5193=VECTOR('',#18640,1.);
#5194=VECTOR('',#18641,1.);
#5195=VECTOR('',#18644,1.);
#5196=VECTOR('',#18645,1.);
#5197=VECTOR('',#18648,1.);
#5198=VECTOR('',#18649,1.);
#5199=VECTOR('',#18650,1.);
#5200=VECTOR('',#18651,1.);
#5201=VECTOR('',#18652,1.);
#5202=VECTOR('',#18653,1.);
#5203=VECTOR('',#18656,1.);
#5204=VECTOR('',#18657,1.);
#5205=VECTOR('',#18658,1.);
#5206=VECTOR('',#18659,1.);
#5207=VECTOR('',#18660,1.);
#5208=VECTOR('',#18663,1.);
#5209=VECTOR('',#18664,1.);
#5210=VECTOR('',#18665,1.);
#5211=VECTOR('',#18666,1.);
#5212=VECTOR('',#18667,1.);
#5213=VECTOR('',#18670,1.);
#5214=VECTOR('',#18671,1.);
#5215=VECTOR('',#18674,1.);
#5216=VECTOR('',#18675,1.);
#5217=VECTOR('',#18676,1.);
#5218=VECTOR('',#18679,1.);
#5219=VECTOR('',#18680,1.);
#5220=VECTOR('',#18681,1.);
#5221=VECTOR('',#18684,1.);
#5222=VECTOR('',#18685,1.);
#5223=VECTOR('',#18686,1.);
#5224=VECTOR('',#18687,1.);
#5225=VECTOR('',#18688,1.);
#5226=VECTOR('',#18691,1.);
#5227=VECTOR('',#18692,1.);
#5228=VECTOR('',#18693,1.);
#5229=VECTOR('',#18694,1.);
#5230=VECTOR('',#18695,1.);
#5231=VECTOR('',#18696,1.);
#5232=VECTOR('',#18697,1.);
#5233=VECTOR('',#18700,1.);
#5234=VECTOR('',#18701,1.);
#5235=VECTOR('',#18704,1.);
#5236=VECTOR('',#18705,1.);
#5237=VECTOR('',#18706,1.);
#5238=VECTOR('',#18707,1.);
#5239=VECTOR('',#18708,1.);
#5240=VECTOR('',#18711,1.);
#5241=VECTOR('',#18712,1.);
#5242=VECTOR('',#18713,1.);
#5243=VECTOR('',#18714,1.);
#5244=VECTOR('',#18717,1.);
#5245=VECTOR('',#18718,1.);
#5246=VECTOR('',#18721,1.);
#5247=VECTOR('',#18724,1.);
#5248=VECTOR('',#18725,1.);
#5249=VECTOR('',#18726,1.);
#5250=VECTOR('',#18729,1.);
#5251=VECTOR('',#18730,1.);
#5252=VECTOR('',#18735,1.);
#5253=VECTOR('',#18736,1.);
#5254=VECTOR('',#18737,1.);
#5255=VECTOR('',#18738,1.);
#5256=VECTOR('',#18741,1.);
#5257=VECTOR('',#18742,1.);
#5258=VECTOR('',#18747,1.);
#5259=VECTOR('',#18748,1.);
#5260=VECTOR('',#18751,1.);
#5261=VECTOR('',#18768,1.);
#5262=VECTOR('',#18771,1.);
#5263=VECTOR('',#18772,1.);
#5264=VECTOR('',#18775,1.);
#5265=VECTOR('',#18776,1.);
#5266=VECTOR('',#18779,1.);
#5267=VECTOR('',#18780,1.);
#5268=VECTOR('',#18781,1.);
#5269=VECTOR('',#18788,1.1106066017178);
#5270=VECTOR('',#18799,1.1);
#5271=VECTOR('',#18802,1.14);
#5272=VECTOR('',#18809,1.115);
#5273=VECTOR('',#18818,1.275);
#5274=VECTOR('',#18829,1.26);
#5275=VECTOR('',#18832,1.37);
#5276=VECTOR('',#18837,1.355);
#5277=VECTOR('',#18840,0.239999999999999);
#5278=VECTOR('',#18849,0.225);
#5279=VECTOR('',#18854,0.239999999999999);
#5280=VECTOR('',#18861,0.240000000000001);
#5281=VECTOR('',#18870,0.225000000000001);
#5282=VECTOR('',#18875,0.240000000000001);
#5283=VECTOR('',#18882,0.27);
#5284=VECTOR('',#18889,0.255);
#5285=VECTOR('',#18892,0.27);
#5286=VECTOR('',#18899,0.255000000000001);
#5287=VECTOR('',#18902,0.27);
#5288=VECTOR('',#18909,0.255);
#5289=VECTOR('',#18914,0.415);
#5290=VECTOR('',#18919,1.);
#5291=VECTOR('',#18920,1.);
#5292=VECTOR('',#18921,1.);
#5293=VECTOR('',#18922,1.);
#5294=VECTOR('',#18935,0.4);
#5295=VECTOR('',#18938,0.415);
#5296=VECTOR('',#18943,0.4);
#5297=VECTOR('',#18946,1.1543933982822);
#5298=VECTOR('',#18949,1.);
#5299=VECTOR('',#18950,1.);
#5300=VECTOR('',#18953,1.);
#5301=VECTOR('',#18956,1.);
#5302=VECTOR('',#18961,0.27);
#5303=VECTOR('',#18964,0.27);
#5304=VECTOR('',#18967,0.27);
#6323=VERTEX_POINT('',#22963);
#6324=VERTEX_POINT('',#22964);
#6325=VERTEX_POINT('',#22966);
#6326=VERTEX_POINT('',#22968);
#6327=VERTEX_POINT('',#22970);
#6328=VERTEX_POINT('',#22972);
#6329=VERTEX_POINT('',#22976);
#6330=VERTEX_POINT('',#22978);
#6331=VERTEX_POINT('',#22980);
#6332=VERTEX_POINT('',#22982);
#6333=VERTEX_POINT('',#22986);
#6334=VERTEX_POINT('',#22988);
#6335=VERTEX_POINT('',#22990);
#6336=VERTEX_POINT('',#22992);
#6337=VERTEX_POINT('',#22994);
#6338=VERTEX_POINT('',#22996);
#6339=VERTEX_POINT('',#23000);
#6340=VERTEX_POINT('',#23004);
#6341=VERTEX_POINT('',#23006);
#6342=VERTEX_POINT('',#23008);
#6343=VERTEX_POINT('',#23010);
#6344=VERTEX_POINT('',#23016);
#6345=VERTEX_POINT('',#23018);
#6346=VERTEX_POINT('',#23020);
#6347=VERTEX_POINT('',#23022);
#6348=VERTEX_POINT('',#23024);
#6349=VERTEX_POINT('',#23028);
#6350=VERTEX_POINT('',#23030);
#6351=VERTEX_POINT('',#23034);
#6352=VERTEX_POINT('',#23036);
#6353=VERTEX_POINT('',#23038);
#6354=VERTEX_POINT('',#23040);
#6355=VERTEX_POINT('',#23042);
#6356=VERTEX_POINT('',#23046);
#6357=VERTEX_POINT('',#23047);
#6358=VERTEX_POINT('',#23050);
#6359=VERTEX_POINT('',#23052);
#6360=VERTEX_POINT('',#23056);
#6361=VERTEX_POINT('',#23058);
#6362=VERTEX_POINT('',#23060);
#6363=VERTEX_POINT('',#23062);
#6364=VERTEX_POINT('',#23066);
#6365=VERTEX_POINT('',#23070);
#6366=VERTEX_POINT('',#23072);
#6367=VERTEX_POINT('',#23076);
#6368=VERTEX_POINT('',#23080);
#6369=VERTEX_POINT('',#23082);
#6370=VERTEX_POINT('',#23084);
#6371=VERTEX_POINT('',#23086);
#6372=VERTEX_POINT('',#23088);
#6373=VERTEX_POINT('',#23092);
#6374=VERTEX_POINT('',#23093);
#6375=VERTEX_POINT('',#23096);
#6376=VERTEX_POINT('',#23098);
#6377=VERTEX_POINT('',#23102);
#6378=VERTEX_POINT('',#23104);
#6379=VERTEX_POINT('',#23106);
#6380=VERTEX_POINT('',#23108);
#6381=VERTEX_POINT('',#23112);
#6382=VERTEX_POINT('',#23116);
#6383=VERTEX_POINT('',#23118);
#6384=VERTEX_POINT('',#23122);
#6385=VERTEX_POINT('',#23124);
#6386=VERTEX_POINT('',#23128);
#6387=VERTEX_POINT('',#23130);
#6388=VERTEX_POINT('',#23132);
#6389=VERTEX_POINT('',#23137);
#6390=VERTEX_POINT('',#23139);
#6391=VERTEX_POINT('',#23141);
#6392=VERTEX_POINT('',#23143);
#6393=VERTEX_POINT('',#23145);
#6394=VERTEX_POINT('',#23147);
#6395=VERTEX_POINT('',#23151);
#6396=VERTEX_POINT('',#23155);
#6397=VERTEX_POINT('',#23157);
#6398=VERTEX_POINT('',#23159);
#6399=VERTEX_POINT('',#23161);
#6400=VERTEX_POINT('',#23166);
#6401=VERTEX_POINT('',#23168);
#6402=VERTEX_POINT('',#23172);
#6403=VERTEX_POINT('',#23178);
#6404=VERTEX_POINT('',#23188);
#6405=VERTEX_POINT('',#23190);
#6406=VERTEX_POINT('',#23194);
#6407=VERTEX_POINT('',#23199);
#6408=VERTEX_POINT('',#23204);
#6409=VERTEX_POINT('',#23206);
#6410=VERTEX_POINT('',#23208);
#6411=VERTEX_POINT('',#23210);
#6412=VERTEX_POINT('',#23212);
#6413=VERTEX_POINT('',#23214);
#6414=VERTEX_POINT('',#23220);
#6415=VERTEX_POINT('',#23224);
#6416=VERTEX_POINT('',#23228);
#6417=VERTEX_POINT('',#23233);
#6418=VERTEX_POINT('',#23234);
#6419=VERTEX_POINT('',#23237);
#6420=VERTEX_POINT('',#23239);
#6421=VERTEX_POINT('',#23243);
#6422=VERTEX_POINT('',#23244);
#6423=VERTEX_POINT('',#23249);
#6424=VERTEX_POINT('',#23253);
#6425=VERTEX_POINT('',#23257);
#6426=VERTEX_POINT('',#23260);
#6427=VERTEX_POINT('',#23262);
#6428=VERTEX_POINT('',#23264);
#6429=VERTEX_POINT('',#23268);
#6430=VERTEX_POINT('',#23273);
#6431=VERTEX_POINT('',#23279);
#6432=VERTEX_POINT('',#23283);
#6433=VERTEX_POINT('',#23284);
#6434=VERTEX_POINT('',#23289);
#6435=VERTEX_POINT('',#23293);
#6436=VERTEX_POINT('',#23296);
#6437=VERTEX_POINT('',#23300);
#6438=VERTEX_POINT('',#23301);
#6439=VERTEX_POINT('',#23306);
#6440=VERTEX_POINT('',#23310);
#6441=VERTEX_POINT('',#23313);
#6442=VERTEX_POINT('',#23317);
#6443=VERTEX_POINT('',#23321);
#6444=VERTEX_POINT('',#23325);
#6445=VERTEX_POINT('',#23329);
#6446=VERTEX_POINT('',#23333);
#6447=VERTEX_POINT('',#23337);
#6448=VERTEX_POINT('',#23339);
#6449=VERTEX_POINT('',#23343);
#6450=VERTEX_POINT('',#23344);
#6451=VERTEX_POINT('',#23346);
#6452=VERTEX_POINT('',#23348);
#6453=VERTEX_POINT('',#23351);
#6454=VERTEX_POINT('',#23353);
#6455=VERTEX_POINT('',#23355);
#6456=VERTEX_POINT('',#23357);
#6457=VERTEX_POINT('',#23359);
#6458=VERTEX_POINT('',#23364);
#7992=EDGE_CURVE('',#6323,#6324,#3915,.T.);
#7993=EDGE_CURVE('',#6324,#6325,#3916,.T.);
#7994=EDGE_CURVE('',#6325,#6326,#3917,.T.);
#7995=EDGE_CURVE('',#6326,#6327,#3918,.T.);
#7996=EDGE_CURVE('',#6327,#6328,#3919,.T.);
#7997=EDGE_CURVE('',#6328,#6323,#3920,.T.);
#7998=EDGE_CURVE('',#6326,#6329,#3921,.T.);
#7999=EDGE_CURVE('',#6329,#6330,#3922,.T.);
#8000=EDGE_CURVE('',#6330,#6331,#3923,.T.);
#8001=EDGE_CURVE('',#6331,#6332,#3924,.T.);
#8002=EDGE_CURVE('',#6332,#6327,#3925,.T.);
#8003=EDGE_CURVE('',#6333,#6325,#3926,.T.);
#8004=EDGE_CURVE('',#6334,#6333,#3927,.T.);
#8005=EDGE_CURVE('',#6335,#6334,#3928,.T.);
#8006=EDGE_CURVE('',#6336,#6335,#3929,.T.);
#8007=EDGE_CURVE('',#6337,#6336,#3930,.T.);
#8008=EDGE_CURVE('',#6338,#6337,#3931,.T.);
#8009=EDGE_CURVE('',#6329,#6338,#3932,.T.);
#8010=EDGE_CURVE('',#6324,#6339,#3933,.T.);
#8011=EDGE_CURVE('',#6333,#6339,#3934,.T.);
#8012=EDGE_CURVE('',#6328,#6340,#3935,.T.);
#8013=EDGE_CURVE('',#6340,#6341,#3936,.T.);
#8014=EDGE_CURVE('',#6341,#6342,#3937,.T.);
#8015=EDGE_CURVE('',#6342,#6343,#3938,.T.);
#8016=EDGE_CURVE('',#6343,#6323,#3939,.T.);
#8017=EDGE_CURVE('',#6340,#6332,#3940,.T.);
#8018=EDGE_CURVE('',#6344,#6343,#3941,.T.);
#8019=EDGE_CURVE('',#6345,#6344,#3942,.T.);
#8020=EDGE_CURVE('',#6346,#6345,#3943,.T.);
#8021=EDGE_CURVE('',#6347,#6346,#3944,.T.);
#8022=EDGE_CURVE('',#6348,#6347,#3945,.T.);
#8023=EDGE_CURVE('',#6339,#6348,#3946,.T.);
#8024=EDGE_CURVE('',#6331,#6349,#3947,.T.);
#8025=EDGE_CURVE('',#6350,#6349,#3948,.T.);
#8026=EDGE_CURVE('',#6350,#6341,#3949,.T.);
#8027=EDGE_CURVE('',#6351,#6330,#3950,.T.);
#8028=EDGE_CURVE('',#6352,#6351,#3951,.T.);
#8029=EDGE_CURVE('',#6353,#6352,#3952,.T.);
#8030=EDGE_CURVE('',#6354,#6353,#3953,.T.);
#8031=EDGE_CURVE('',#6355,#6354,#3954,.T.);
#8032=EDGE_CURVE('',#6349,#6355,#3955,.T.);
#8033=EDGE_CURVE('',#6356,#6357,#3956,.T.);
#8034=EDGE_CURVE('',#6357,#6346,#3957,.T.);
#8035=EDGE_CURVE('',#6345,#6358,#3958,.T.);
#8036=EDGE_CURVE('',#6358,#6359,#3959,.T.);
#8037=EDGE_CURVE('',#6359,#6356,#3960,.T.);
#8038=EDGE_CURVE('',#6359,#6360,#3961,.T.);
#8039=EDGE_CURVE('',#6360,#6361,#3962,.T.);
#8040=EDGE_CURVE('',#6361,#6362,#3963,.T.);
#8041=EDGE_CURVE('',#6362,#6363,#3964,.T.);
#8042=EDGE_CURVE('',#6363,#6356,#3965,.T.);
#8043=EDGE_CURVE('',#6364,#6358,#3966,.T.);
#8044=EDGE_CURVE('',#6360,#6364,#3967,.T.);
#8045=EDGE_CURVE('',#6344,#6365,#3968,.T.);
#8046=EDGE_CURVE('',#6365,#6366,#3969,.T.);
#8047=EDGE_CURVE('',#6366,#6364,#3970,.T.);
#8048=EDGE_CURVE('',#6357,#6367,#3971,.T.);
#8049=EDGE_CURVE('',#6347,#6367,#3972,.T.);
#8050=EDGE_CURVE('',#6368,#6363,#3973,.T.);
#8051=EDGE_CURVE('',#6369,#6368,#3974,.T.);
#8052=EDGE_CURVE('',#6370,#6369,#3975,.T.);
#8053=EDGE_CURVE('',#6371,#6370,#3976,.T.);
#8054=EDGE_CURVE('',#6372,#6371,#3977,.T.);
#8055=EDGE_CURVE('',#6367,#6372,#3978,.T.);
#8056=EDGE_CURVE('',#6373,#6374,#3979,.T.);
#8057=EDGE_CURVE('',#6374,#6370,#3980,.T.);
#8058=EDGE_CURVE('',#6369,#6375,#3981,.T.);
#8059=EDGE_CURVE('',#6375,#6376,#3982,.T.);
#8060=EDGE_CURVE('',#6376,#6373,#3983,.T.);
#8061=EDGE_CURVE('',#6376,#6377,#3984,.T.);
#8062=EDGE_CURVE('',#6377,#6378,#3985,.T.);
#8063=EDGE_CURVE('',#6378,#6379,#3986,.T.);
#8064=EDGE_CURVE('',#6379,#6380,#3987,.T.);
#8065=EDGE_CURVE('',#6380,#6373,#3988,.T.);
#8066=EDGE_CURVE('',#6381,#6375,#3989,.T.);
#8067=EDGE_CURVE('',#6377,#6381,#3990,.T.);
#8068=EDGE_CURVE('',#6368,#6382,#3991,.T.);
#8069=EDGE_CURVE('',#6382,#6383,#3992,.T.);
#8070=EDGE_CURVE('',#6383,#6381,#3993,.T.);
#8071=EDGE_CURVE('',#6383,#6384,#3994,.T.);
#8072=EDGE_CURVE('',#6385,#6384,#3995,.T.);
#8073=EDGE_CURVE('',#6385,#6378,#3996,.T.);
#8074=EDGE_CURVE('',#6386,#6361,#3997,.T.);
#8075=EDGE_CURVE('',#6387,#6386,#3998,.T.);
#8076=EDGE_CURVE('',#6388,#6387,#3999,.T.);
#8077=EDGE_CURVE('',#6384,#6388,#4000,.T.);
#8078=EDGE_CURVE('',#6362,#6382,#4001,.T.);
#8079=EDGE_CURVE('',#6389,#6380,#4002,.T.);
#8080=EDGE_CURVE('',#6390,#6389,#4003,.T.);
#8081=EDGE_CURVE('',#6391,#6390,#4004,.T.);
#8082=EDGE_CURVE('',#6392,#6391,#4005,.T.);
#8083=EDGE_CURVE('',#6393,#6392,#4006,.T.);
#8084=EDGE_CURVE('',#6394,#6393,#4007,.T.);
#8085=EDGE_CURVE('',#6374,#6394,#4008,.T.);
#8086=EDGE_CURVE('',#6379,#6395,#4009,.T.);
#8087=EDGE_CURVE('',#6389,#6395,#4010,.T.);
#8088=EDGE_CURVE('',#6396,#6385,#4011,.T.);
#8089=EDGE_CURVE('',#6397,#6396,#4012,.T.);
#8090=EDGE_CURVE('',#6398,#6397,#4013,.T.);
#8091=EDGE_CURVE('',#6399,#6398,#4014,.T.);
#8092=EDGE_CURVE('',#6395,#6399,#4015,.T.);
#8093=EDGE_CURVE('',#6336,#6391,#4016,.T.);
#8094=EDGE_CURVE('',#6390,#6400,#4017,.T.);
#8095=EDGE_CURVE('',#6400,#6401,#4018,.T.);
#8096=EDGE_CURVE('',#6401,#6337,#4019,.T.);
#8097=EDGE_CURVE('',#6399,#6402,#4020,.T.);
#8098=EDGE_CURVE('',#6402,#6400,#4021,.T.);
#8099=EDGE_CURVE('',#6392,#6335,#4022,.T.);
#8100=EDGE_CURVE('',#6401,#6403,#4023,.T.);
#8101=EDGE_CURVE('',#6403,#6352,#4024,.T.);
#8102=EDGE_CURVE('',#6351,#6338,#4025,.T.);
#8103=EDGE_CURVE('',#6403,#6402,#4026,.T.);
#8104=EDGE_CURVE('',#6398,#6353,#4027,.T.);
#8105=EDGE_CURVE('',#6371,#6394,#4028,.T.);
#8106=EDGE_CURVE('',#6393,#6404,#4029,.T.);
#8107=EDGE_CURVE('',#6404,#6405,#4030,.T.);
#8108=EDGE_CURVE('',#6405,#6372,#4031,.T.);
#8109=EDGE_CURVE('',#6406,#6334,#4032,.T.);
#8110=EDGE_CURVE('',#6406,#6404,#4033,.T.);
#8111=EDGE_CURVE('',#6348,#6407,#4034,.T.);
#8112=EDGE_CURVE('',#6407,#6406,#4035,.T.);
#8113=EDGE_CURVE('',#6405,#6407,#4036,.T.);
#8114=EDGE_CURVE('',#6408,#6408,#1293,.T.);
#8115=EDGE_CURVE('',#6409,#6409,#1294,.T.);
#8116=EDGE_CURVE('',#6410,#6410,#1295,.T.);
#8117=EDGE_CURVE('',#6411,#6411,#1296,.T.);
#8118=EDGE_CURVE('',#6412,#6412,#1297,.T.);
#8119=EDGE_CURVE('',#6413,#6413,#1298,.T.);
#8120=EDGE_CURVE('',#6354,#6397,#4037,.T.);
#8121=EDGE_CURVE('',#6366,#6414,#4038,.T.);
#8122=EDGE_CURVE('',#6414,#6386,#4039,.T.);
#8123=EDGE_CURVE('',#6414,#6415,#4040,.T.);
#8124=EDGE_CURVE('',#6387,#6415,#4041,.T.);
#8125=EDGE_CURVE('',#6416,#6350,#4042,.T.);
#8126=EDGE_CURVE('',#6415,#6416,#4043,.T.);
#8127=EDGE_CURVE('',#6342,#6365,#4044,.T.);
#8128=EDGE_CURVE('',#6417,#6418,#1299,.T.);
#8129=EDGE_CURVE('',#6418,#6417,#1300,.T.);
#8130=EDGE_CURVE('',#6417,#6419,#4045,.T.);
#8131=EDGE_CURVE('',#6419,#6420,#1301,.T.);
#8132=EDGE_CURVE('',#6420,#6419,#1302,.T.);
#8133=EDGE_CURVE('',#6421,#6422,#1303,.T.);
#8134=EDGE_CURVE('',#6422,#6421,#1304,.T.);
#8135=EDGE_CURVE('',#6422,#6418,#4046,.T.);
#8136=EDGE_CURVE('',#6420,#6423,#4047,.T.);
#8137=EDGE_CURVE('',#6423,#6423,#1305,.T.);
#8138=EDGE_CURVE('',#6424,#6424,#1306,.T.);
#8139=EDGE_CURVE('',#6424,#6421,#4048,.T.);
#8140=EDGE_CURVE('',#6425,#6425,#1307,.T.);
#8141=EDGE_CURVE('',#6426,#6426,#1308,.T.);
#8142=EDGE_CURVE('',#6426,#6427,#4049,.T.);
#8143=EDGE_CURVE('',#6427,#6428,#1309,.T.);
#8144=EDGE_CURVE('',#6428,#6427,#1310,.T.);
#8145=EDGE_CURVE('',#6429,#6429,#1311,.T.);
#8146=EDGE_CURVE('',#6428,#6425,#4050,.T.);
#8147=EDGE_CURVE('',#6413,#6430,#4051,.T.);
#8148=EDGE_CURVE('',#6430,#6430,#1312,.T.);
#8149=EDGE_CURVE('',#6430,#6429,#4052,.T.);
#8150=EDGE_CURVE('',#6408,#6431,#4053,.T.);
#8151=EDGE_CURVE('',#6431,#6431,#1313,.T.);
#8152=EDGE_CURVE('',#6432,#6433,#1314,.T.);
#8153=EDGE_CURVE('',#6433,#6432,#1315,.T.);
#8154=EDGE_CURVE('',#6433,#6431,#4054,.T.);
#8155=EDGE_CURVE('',#6434,#6434,#1316,.T.);
#8156=EDGE_CURVE('',#6434,#6432,#4055,.T.);
#8157=EDGE_CURVE('',#6435,#6435,#1317,.T.);
#8158=EDGE_CURVE('',#6412,#6436,#4056,.T.);
#8159=EDGE_CURVE('',#6436,#6436,#1318,.T.);
#8160=EDGE_CURVE('',#6437,#6438,#1319,.T.);
#8161=EDGE_CURVE('',#6438,#6437,#1320,.T.);
#8162=EDGE_CURVE('',#6438,#6436,#4057,.T.);
#8163=EDGE_CURVE('',#6439,#6439,#1321,.T.);
#8164=EDGE_CURVE('',#6439,#6437,#4058,.T.);
#8165=EDGE_CURVE('',#6440,#6440,#1322,.T.);
#8166=EDGE_CURVE('',#6409,#6441,#4059,.T.);
#8167=EDGE_CURVE('',#6441,#6441,#1323,.T.);
#8168=EDGE_CURVE('',#6442,#6442,#1324,.T.);
#8169=EDGE_CURVE('',#6442,#6441,#4060,.T.);
#8170=EDGE_CURVE('',#6411,#6443,#4061,.T.);
#8171=EDGE_CURVE('',#6443,#6443,#1325,.T.);
#8172=EDGE_CURVE('',#6444,#6444,#1326,.T.);
#8173=EDGE_CURVE('',#6444,#6443,#4062,.T.);
#8174=EDGE_CURVE('',#6410,#6445,#4063,.T.);
#8175=EDGE_CURVE('',#6445,#6445,#1327,.T.);
#8176=EDGE_CURVE('',#6446,#6446,#1328,.T.);
#8177=EDGE_CURVE('',#6446,#6445,#4064,.T.);
#8178=EDGE_CURVE('',#6447,#6447,#1329,.T.);
#8179=EDGE_CURVE('',#6447,#6448,#4065,.T.);
#8180=EDGE_CURVE('',#6448,#6448,#1330,.T.);
#8181=EDGE_CURVE('',#6449,#6450,#4066,.T.);
#8182=EDGE_CURVE('',#6451,#6449,#4067,.T.);
#8183=EDGE_CURVE('',#6452,#6451,#4068,.T.);
#8184=EDGE_CURVE('',#6450,#6452,#4069,.T.);
#8185=EDGE_CURVE('',#6453,#6453,#1331,.T.);
#8186=EDGE_CURVE('',#6454,#6454,#1332,.T.);
#8187=EDGE_CURVE('',#6455,#6455,#1333,.T.);
#8188=EDGE_CURVE('',#6456,#6456,#1334,.T.);
#8189=EDGE_CURVE('',#6457,#6457,#1335,.T.);
#8190=EDGE_CURVE('',#6448,#6440,#4070,.T.);
#8191=EDGE_CURVE('',#6453,#6458,#4071,.T.);
#8192=EDGE_CURVE('',#6458,#6458,#1336,.T.);
#8193=EDGE_CURVE('',#6458,#6435,#4072,.T.);
#8194=EDGE_CURVE('',#6457,#6423,#4073,.T.);
#8195=EDGE_CURVE('',#6355,#6449,#4074,.T.);
#8196=EDGE_CURVE('',#6450,#6416,#4075,.T.);
#8197=EDGE_CURVE('',#6451,#6396,#4076,.T.);
#8198=EDGE_CURVE('',#6388,#6452,#4077,.T.);
#8199=EDGE_CURVE('',#6454,#6446,#4078,.T.);
#8200=EDGE_CURVE('',#6456,#6444,#4079,.T.);
#8201=EDGE_CURVE('',#6455,#6442,#4080,.T.);
#10753=ORIENTED_EDGE('',*,*,#7992,.T.);
#10754=ORIENTED_EDGE('',*,*,#7993,.T.);
#10755=ORIENTED_EDGE('',*,*,#7994,.T.);
#10756=ORIENTED_EDGE('',*,*,#7995,.T.);
#10757=ORIENTED_EDGE('',*,*,#7996,.T.);
#10758=ORIENTED_EDGE('',*,*,#7997,.T.);
#10759=ORIENTED_EDGE('',*,*,#7995,.F.);
#10760=ORIENTED_EDGE('',*,*,#7998,.T.);
#10761=ORIENTED_EDGE('',*,*,#7999,.T.);
#10762=ORIENTED_EDGE('',*,*,#8000,.T.);
#10763=ORIENTED_EDGE('',*,*,#8001,.T.);
#10764=ORIENTED_EDGE('',*,*,#8002,.T.);
#10765=ORIENTED_EDGE('',*,*,#7994,.F.);
#10766=ORIENTED_EDGE('',*,*,#8003,.F.);
#10767=ORIENTED_EDGE('',*,*,#8004,.F.);
#10768=ORIENTED_EDGE('',*,*,#8005,.F.);
#10769=ORIENTED_EDGE('',*,*,#8006,.F.);
#10770=ORIENTED_EDGE('',*,*,#8007,.F.);
#10771=ORIENTED_EDGE('',*,*,#8008,.F.);
#10772=ORIENTED_EDGE('',*,*,#8009,.F.);
#10773=ORIENTED_EDGE('',*,*,#7998,.F.);
#10774=ORIENTED_EDGE('',*,*,#7993,.F.);
#10775=ORIENTED_EDGE('',*,*,#8010,.T.);
#10776=ORIENTED_EDGE('',*,*,#8011,.F.);
#10777=ORIENTED_EDGE('',*,*,#8003,.T.);
#10778=ORIENTED_EDGE('',*,*,#7997,.F.);
#10779=ORIENTED_EDGE('',*,*,#8012,.T.);
#10780=ORIENTED_EDGE('',*,*,#8013,.T.);
#10781=ORIENTED_EDGE('',*,*,#8014,.T.);
#10782=ORIENTED_EDGE('',*,*,#8015,.T.);
#10783=ORIENTED_EDGE('',*,*,#8016,.T.);
#10784=ORIENTED_EDGE('',*,*,#7996,.F.);
#10785=ORIENTED_EDGE('',*,*,#8002,.F.);
#10786=ORIENTED_EDGE('',*,*,#8017,.F.);
#10787=ORIENTED_EDGE('',*,*,#8012,.F.);
#10788=ORIENTED_EDGE('',*,*,#7992,.F.);
#10789=ORIENTED_EDGE('',*,*,#8016,.F.);
#10790=ORIENTED_EDGE('',*,*,#8018,.F.);
#10791=ORIENTED_EDGE('',*,*,#8019,.F.);
#10792=ORIENTED_EDGE('',*,*,#8020,.F.);
#10793=ORIENTED_EDGE('',*,*,#8021,.F.);
#10794=ORIENTED_EDGE('',*,*,#8022,.F.);
#10795=ORIENTED_EDGE('',*,*,#8023,.F.);
#10796=ORIENTED_EDGE('',*,*,#8010,.F.);
#10797=ORIENTED_EDGE('',*,*,#8013,.F.);
#10798=ORIENTED_EDGE('',*,*,#8017,.T.);
#10799=ORIENTED_EDGE('',*,*,#8001,.F.);
#10800=ORIENTED_EDGE('',*,*,#8024,.T.);
#10801=ORIENTED_EDGE('',*,*,#8025,.F.);
#10802=ORIENTED_EDGE('',*,*,#8026,.T.);
#10803=ORIENTED_EDGE('',*,*,#8000,.F.);
#10804=ORIENTED_EDGE('',*,*,#8027,.F.);
#10805=ORIENTED_EDGE('',*,*,#8028,.F.);
#10806=ORIENTED_EDGE('',*,*,#8029,.F.);
#10807=ORIENTED_EDGE('',*,*,#8030,.F.);
#10808=ORIENTED_EDGE('',*,*,#8031,.F.);
#10809=ORIENTED_EDGE('',*,*,#8032,.F.);
#10810=ORIENTED_EDGE('',*,*,#8024,.F.);
#10811=ORIENTED_EDGE('',*,*,#8033,.T.);
#10812=ORIENTED_EDGE('',*,*,#8034,.T.);
#10813=ORIENTED_EDGE('',*,*,#8020,.T.);
#10814=ORIENTED_EDGE('',*,*,#8035,.T.);
#10815=ORIENTED_EDGE('',*,*,#8036,.T.);
#10816=ORIENTED_EDGE('',*,*,#8037,.T.);
#10817=ORIENTED_EDGE('',*,*,#8037,.F.);
#10818=ORIENTED_EDGE('',*,*,#8038,.T.);
#10819=ORIENTED_EDGE('',*,*,#8039,.T.);
#10820=ORIENTED_EDGE('',*,*,#8040,.T.);
#10821=ORIENTED_EDGE('',*,*,#8041,.T.);
#10822=ORIENTED_EDGE('',*,*,#8042,.T.);
#10823=ORIENTED_EDGE('',*,*,#8036,.F.);
#10824=ORIENTED_EDGE('',*,*,#8043,.F.);
#10825=ORIENTED_EDGE('',*,*,#8044,.F.);
#10826=ORIENTED_EDGE('',*,*,#8038,.F.);
#10827=ORIENTED_EDGE('',*,*,#8035,.F.);
#10828=ORIENTED_EDGE('',*,*,#8019,.T.);
#10829=ORIENTED_EDGE('',*,*,#8045,.T.);
#10830=ORIENTED_EDGE('',*,*,#8046,.T.);
#10831=ORIENTED_EDGE('',*,*,#8047,.T.);
#10832=ORIENTED_EDGE('',*,*,#8043,.T.);
#10833=ORIENTED_EDGE('',*,*,#8034,.F.);
#10834=ORIENTED_EDGE('',*,*,#8048,.T.);
#10835=ORIENTED_EDGE('',*,*,#8049,.F.);
#10836=ORIENTED_EDGE('',*,*,#8021,.T.);
#10837=ORIENTED_EDGE('',*,*,#8033,.F.);
#10838=ORIENTED_EDGE('',*,*,#8042,.F.);
#10839=ORIENTED_EDGE('',*,*,#8050,.F.);
#10840=ORIENTED_EDGE('',*,*,#8051,.F.);
#10841=ORIENTED_EDGE('',*,*,#8052,.F.);
#10842=ORIENTED_EDGE('',*,*,#8053,.F.);
#10843=ORIENTED_EDGE('',*,*,#8054,.F.);
#10844=ORIENTED_EDGE('',*,*,#8055,.F.);
#10845=ORIENTED_EDGE('',*,*,#8048,.F.);
#10846=ORIENTED_EDGE('',*,*,#8056,.T.);
#10847=ORIENTED_EDGE('',*,*,#8057,.T.);
#10848=ORIENTED_EDGE('',*,*,#8052,.T.);
#10849=ORIENTED_EDGE('',*,*,#8058,.T.);
#10850=ORIENTED_EDGE('',*,*,#8059,.T.);
#10851=ORIENTED_EDGE('',*,*,#8060,.T.);
#10852=ORIENTED_EDGE('',*,*,#8060,.F.);
#10853=ORIENTED_EDGE('',*,*,#8061,.T.);
#10854=ORIENTED_EDGE('',*,*,#8062,.T.);
#10855=ORIENTED_EDGE('',*,*,#8063,.T.);
#10856=ORIENTED_EDGE('',*,*,#8064,.T.);
#10857=ORIENTED_EDGE('',*,*,#8065,.T.);
#10858=ORIENTED_EDGE('',*,*,#8059,.F.);
#10859=ORIENTED_EDGE('',*,*,#8066,.F.);
#10860=ORIENTED_EDGE('',*,*,#8067,.F.);
#10861=ORIENTED_EDGE('',*,*,#8061,.F.);
#10862=ORIENTED_EDGE('',*,*,#8058,.F.);
#10863=ORIENTED_EDGE('',*,*,#8051,.T.);
#10864=ORIENTED_EDGE('',*,*,#8068,.T.);
#10865=ORIENTED_EDGE('',*,*,#8069,.T.);
#10866=ORIENTED_EDGE('',*,*,#8070,.T.);
#10867=ORIENTED_EDGE('',*,*,#8066,.T.);
#10868=ORIENTED_EDGE('',*,*,#8070,.F.);
#10869=ORIENTED_EDGE('',*,*,#8071,.T.);
#10870=ORIENTED_EDGE('',*,*,#8072,.F.);
#10871=ORIENTED_EDGE('',*,*,#8073,.T.);
#10872=ORIENTED_EDGE('',*,*,#8062,.F.);
#10873=ORIENTED_EDGE('',*,*,#8067,.T.);
#10874=ORIENTED_EDGE('',*,*,#8040,.F.);
#10875=ORIENTED_EDGE('',*,*,#8074,.F.);
#10876=ORIENTED_EDGE('',*,*,#8075,.F.);
#10877=ORIENTED_EDGE('',*,*,#8076,.F.);
#10878=ORIENTED_EDGE('',*,*,#8077,.F.);
#10879=ORIENTED_EDGE('',*,*,#8071,.F.);
#10880=ORIENTED_EDGE('',*,*,#8069,.F.);
#10881=ORIENTED_EDGE('',*,*,#8078,.F.);
#10882=ORIENTED_EDGE('',*,*,#8056,.F.);
#10883=ORIENTED_EDGE('',*,*,#8065,.F.);
#10884=ORIENTED_EDGE('',*,*,#8079,.F.);
#10885=ORIENTED_EDGE('',*,*,#8080,.F.);
#10886=ORIENTED_EDGE('',*,*,#8081,.F.);
#10887=ORIENTED_EDGE('',*,*,#8082,.F.);
#10888=ORIENTED_EDGE('',*,*,#8083,.F.);
#10889=ORIENTED_EDGE('',*,*,#8084,.F.);
#10890=ORIENTED_EDGE('',*,*,#8085,.F.);
#10891=ORIENTED_EDGE('',*,*,#8064,.F.);
#10892=ORIENTED_EDGE('',*,*,#8086,.T.);
#10893=ORIENTED_EDGE('',*,*,#8087,.F.);
#10894=ORIENTED_EDGE('',*,*,#8079,.T.);
#10895=ORIENTED_EDGE('',*,*,#8063,.F.);
#10896=ORIENTED_EDGE('',*,*,#8073,.F.);
#10897=ORIENTED_EDGE('',*,*,#8088,.F.);
#10898=ORIENTED_EDGE('',*,*,#8089,.F.);
#10899=ORIENTED_EDGE('',*,*,#8090,.F.);
#10900=ORIENTED_EDGE('',*,*,#8091,.F.);
#10901=ORIENTED_EDGE('',*,*,#8092,.F.);
#10902=ORIENTED_EDGE('',*,*,#8086,.F.);
#10903=ORIENTED_EDGE('',*,*,#8007,.T.);
#10904=ORIENTED_EDGE('',*,*,#8093,.T.);
#10905=ORIENTED_EDGE('',*,*,#8081,.T.);
#10906=ORIENTED_EDGE('',*,*,#8094,.T.);
#10907=ORIENTED_EDGE('',*,*,#8095,.T.);
#10908=ORIENTED_EDGE('',*,*,#8096,.T.);
#10909=ORIENTED_EDGE('',*,*,#8094,.F.);
#10910=ORIENTED_EDGE('',*,*,#8080,.T.);
#10911=ORIENTED_EDGE('',*,*,#8087,.T.);
#10912=ORIENTED_EDGE('',*,*,#8092,.T.);
#10913=ORIENTED_EDGE('',*,*,#8097,.T.);
#10914=ORIENTED_EDGE('',*,*,#8098,.T.);
#10915=ORIENTED_EDGE('',*,*,#8093,.F.);
#10916=ORIENTED_EDGE('',*,*,#8006,.T.);
#10917=ORIENTED_EDGE('',*,*,#8099,.F.);
#10918=ORIENTED_EDGE('',*,*,#8082,.T.);
#10919=ORIENTED_EDGE('',*,*,#8096,.F.);
#10920=ORIENTED_EDGE('',*,*,#8100,.T.);
#10921=ORIENTED_EDGE('',*,*,#8101,.T.);
#10922=ORIENTED_EDGE('',*,*,#8028,.T.);
#10923=ORIENTED_EDGE('',*,*,#8102,.T.);
#10924=ORIENTED_EDGE('',*,*,#8008,.T.);
#10925=ORIENTED_EDGE('',*,*,#8101,.F.);
#10926=ORIENTED_EDGE('',*,*,#8103,.T.);
#10927=ORIENTED_EDGE('',*,*,#8097,.F.);
#10928=ORIENTED_EDGE('',*,*,#8091,.T.);
#10929=ORIENTED_EDGE('',*,*,#8104,.T.);
#10930=ORIENTED_EDGE('',*,*,#8029,.T.);
#10931=ORIENTED_EDGE('',*,*,#8095,.F.);
#10932=ORIENTED_EDGE('',*,*,#8098,.F.);
#10933=ORIENTED_EDGE('',*,*,#8103,.F.);
#10934=ORIENTED_EDGE('',*,*,#8100,.F.);
#10935=ORIENTED_EDGE('',*,*,#8054,.T.);
#10936=ORIENTED_EDGE('',*,*,#8105,.T.);
#10937=ORIENTED_EDGE('',*,*,#8084,.T.);
#10938=ORIENTED_EDGE('',*,*,#8106,.T.);
#10939=ORIENTED_EDGE('',*,*,#8107,.T.);
#10940=ORIENTED_EDGE('',*,*,#8108,.T.);
#10941=ORIENTED_EDGE('',*,*,#8106,.F.);
#10942=ORIENTED_EDGE('',*,*,#8083,.T.);
#10943=ORIENTED_EDGE('',*,*,#8099,.T.);
#10944=ORIENTED_EDGE('',*,*,#8005,.T.);
#10945=ORIENTED_EDGE('',*,*,#8109,.F.);
#10946=ORIENTED_EDGE('',*,*,#8110,.T.);
#10947=ORIENTED_EDGE('',*,*,#8057,.F.);
#10948=ORIENTED_EDGE('',*,*,#8085,.T.);
#10949=ORIENTED_EDGE('',*,*,#8105,.F.);
#10950=ORIENTED_EDGE('',*,*,#8053,.T.);
#10951=ORIENTED_EDGE('',*,*,#8004,.T.);
#10952=ORIENTED_EDGE('',*,*,#8011,.T.);
#10953=ORIENTED_EDGE('',*,*,#8023,.T.);
#10954=ORIENTED_EDGE('',*,*,#8111,.T.);
#10955=ORIENTED_EDGE('',*,*,#8112,.T.);
#10956=ORIENTED_EDGE('',*,*,#8109,.T.);
#10957=ORIENTED_EDGE('',*,*,#8107,.F.);
#10958=ORIENTED_EDGE('',*,*,#8110,.F.);
#10959=ORIENTED_EDGE('',*,*,#8112,.F.);
#10960=ORIENTED_EDGE('',*,*,#8113,.F.);
#10961=ORIENTED_EDGE('',*,*,#8114,.F.);
#10962=ORIENTED_EDGE('',*,*,#8115,.F.);
#10963=ORIENTED_EDGE('',*,*,#8116,.F.);
#10964=ORIENTED_EDGE('',*,*,#8117,.F.);
#10965=ORIENTED_EDGE('',*,*,#8118,.F.);
#10966=ORIENTED_EDGE('',*,*,#8119,.F.);
#10967=ORIENTED_EDGE('',*,*,#8108,.F.);
#10968=ORIENTED_EDGE('',*,*,#8113,.T.);
#10969=ORIENTED_EDGE('',*,*,#8111,.F.);
#10970=ORIENTED_EDGE('',*,*,#8022,.T.);
#10971=ORIENTED_EDGE('',*,*,#8049,.T.);
#10972=ORIENTED_EDGE('',*,*,#8055,.T.);
#10973=ORIENTED_EDGE('',*,*,#8104,.F.);
#10974=ORIENTED_EDGE('',*,*,#8090,.T.);
#10975=ORIENTED_EDGE('',*,*,#8120,.F.);
#10976=ORIENTED_EDGE('',*,*,#8030,.T.);
#10977=ORIENTED_EDGE('',*,*,#8047,.F.);
#10978=ORIENTED_EDGE('',*,*,#8121,.T.);
#10979=ORIENTED_EDGE('',*,*,#8122,.T.);
#10980=ORIENTED_EDGE('',*,*,#8074,.T.);
#10981=ORIENTED_EDGE('',*,*,#8039,.F.);
#10982=ORIENTED_EDGE('',*,*,#8044,.T.);
#10983=ORIENTED_EDGE('',*,*,#8122,.F.);
#10984=ORIENTED_EDGE('',*,*,#8123,.T.);
#10985=ORIENTED_EDGE('',*,*,#8124,.F.);
#10986=ORIENTED_EDGE('',*,*,#8075,.T.);
#10987=ORIENTED_EDGE('',*,*,#8014,.F.);
#10988=ORIENTED_EDGE('',*,*,#8026,.F.);
#10989=ORIENTED_EDGE('',*,*,#8125,.F.);
#10990=ORIENTED_EDGE('',*,*,#8126,.F.);
#10991=ORIENTED_EDGE('',*,*,#8123,.F.);
#10992=ORIENTED_EDGE('',*,*,#8121,.F.);
#10993=ORIENTED_EDGE('',*,*,#8046,.F.);
#10994=ORIENTED_EDGE('',*,*,#8127,.F.);
#10995=ORIENTED_EDGE('',*,*,#8128,.T.);
#10996=ORIENTED_EDGE('',*,*,#8129,.T.);
#10997=ORIENTED_EDGE('',*,*,#8130,.T.);
#10998=ORIENTED_EDGE('',*,*,#8131,.T.);
#10999=ORIENTED_EDGE('',*,*,#8132,.T.);
#11000=ORIENTED_EDGE('',*,*,#8130,.F.);
#11001=ORIENTED_EDGE('',*,*,#8133,.F.);
#11002=ORIENTED_EDGE('',*,*,#8134,.F.);
#11003=ORIENTED_EDGE('',*,*,#8135,.T.);
#11004=ORIENTED_EDGE('',*,*,#8128,.F.);
#11005=ORIENTED_EDGE('',*,*,#8129,.F.);
#11006=ORIENTED_EDGE('',*,*,#8135,.F.);
#11007=ORIENTED_EDGE('',*,*,#8131,.F.);
#11008=ORIENTED_EDGE('',*,*,#8132,.F.);
#11009=ORIENTED_EDGE('',*,*,#8136,.T.);
#11010=ORIENTED_EDGE('',*,*,#8137,.F.);
#11011=ORIENTED_EDGE('',*,*,#8136,.F.);
#11012=ORIENTED_EDGE('',*,*,#8138,.T.);
#11013=ORIENTED_EDGE('',*,*,#8139,.T.);
#11014=ORIENTED_EDGE('',*,*,#8133,.T.);
#11015=ORIENTED_EDGE('',*,*,#8134,.T.);
#11016=ORIENTED_EDGE('',*,*,#8139,.F.);
#11017=ORIENTED_EDGE('',*,*,#8140,.F.);
#11018=ORIENTED_EDGE('',*,*,#8138,.F.);
#11019=ORIENTED_EDGE('',*,*,#8141,.T.);
#11020=ORIENTED_EDGE('',*,*,#8142,.T.);
#11021=ORIENTED_EDGE('',*,*,#8143,.T.);
#11022=ORIENTED_EDGE('',*,*,#8144,.T.);
#11023=ORIENTED_EDGE('',*,*,#8142,.F.);
#11024=ORIENTED_EDGE('',*,*,#8145,.F.);
#11025=ORIENTED_EDGE('',*,*,#8141,.F.);
#11026=ORIENTED_EDGE('',*,*,#8143,.F.);
#11027=ORIENTED_EDGE('',*,*,#8144,.F.);
#11028=ORIENTED_EDGE('',*,*,#8146,.T.);
#11029=ORIENTED_EDGE('',*,*,#8140,.T.);
#11030=ORIENTED_EDGE('',*,*,#8146,.F.);
#11031=ORIENTED_EDGE('',*,*,#8119,.T.);
#11032=ORIENTED_EDGE('',*,*,#8147,.T.);
#11033=ORIENTED_EDGE('',*,*,#8148,.T.);
#11034=ORIENTED_EDGE('',*,*,#8147,.F.);
#11035=ORIENTED_EDGE('',*,*,#8148,.F.);
#11036=ORIENTED_EDGE('',*,*,#8149,.T.);
#11037=ORIENTED_EDGE('',*,*,#8145,.T.);
#11038=ORIENTED_EDGE('',*,*,#8149,.F.);
#11039=ORIENTED_EDGE('',*,*,#8114,.T.);
#11040=ORIENTED_EDGE('',*,*,#8150,.T.);
#11041=ORIENTED_EDGE('',*,*,#8151,.T.);
#11042=ORIENTED_EDGE('',*,*,#8150,.F.);
#11043=ORIENTED_EDGE('',*,*,#8152,.F.);
#11044=ORIENTED_EDGE('',*,*,#8153,.F.);
#11045=ORIENTED_EDGE('',*,*,#8154,.T.);
#11046=ORIENTED_EDGE('',*,*,#8151,.F.);
#11047=ORIENTED_EDGE('',*,*,#8154,.F.);
#11048=ORIENTED_EDGE('',*,*,#8155,.T.);
#11049=ORIENTED_EDGE('',*,*,#8156,.T.);
#11050=ORIENTED_EDGE('',*,*,#8152,.T.);
#11051=ORIENTED_EDGE('',*,*,#8153,.T.);
#11052=ORIENTED_EDGE('',*,*,#8156,.F.);
#11053=ORIENTED_EDGE('',*,*,#8157,.F.);
#11054=ORIENTED_EDGE('',*,*,#8155,.F.);
#11055=ORIENTED_EDGE('',*,*,#8118,.T.);
#11056=ORIENTED_EDGE('',*,*,#8158,.T.);
#11057=ORIENTED_EDGE('',*,*,#8159,.T.);
#11058=ORIENTED_EDGE('',*,*,#8158,.F.);
#11059=ORIENTED_EDGE('',*,*,#8160,.F.);
#11060=ORIENTED_EDGE('',*,*,#8161,.F.);
#11061=ORIENTED_EDGE('',*,*,#8162,.T.);
#11062=ORIENTED_EDGE('',*,*,#8159,.F.);
#11063=ORIENTED_EDGE('',*,*,#8162,.F.);
#11064=ORIENTED_EDGE('',*,*,#8163,.T.);
#11065=ORIENTED_EDGE('',*,*,#8164,.T.);
#11066=ORIENTED_EDGE('',*,*,#8160,.T.);
#11067=ORIENTED_EDGE('',*,*,#8161,.T.);
#11068=ORIENTED_EDGE('',*,*,#8164,.F.);
#11069=ORIENTED_EDGE('',*,*,#8165,.F.);
#11070=ORIENTED_EDGE('',*,*,#8163,.F.);
#11071=ORIENTED_EDGE('',*,*,#8115,.T.);
#11072=ORIENTED_EDGE('',*,*,#8166,.T.);
#11073=ORIENTED_EDGE('',*,*,#8167,.T.);
#11074=ORIENTED_EDGE('',*,*,#8166,.F.);
#11075=ORIENTED_EDGE('',*,*,#8168,.F.);
#11076=ORIENTED_EDGE('',*,*,#8169,.T.);
#11077=ORIENTED_EDGE('',*,*,#8167,.F.);
#11078=ORIENTED_EDGE('',*,*,#8169,.F.);
#11079=ORIENTED_EDGE('',*,*,#8117,.T.);
#11080=ORIENTED_EDGE('',*,*,#8170,.T.);
#11081=ORIENTED_EDGE('',*,*,#8171,.T.);
#11082=ORIENTED_EDGE('',*,*,#8170,.F.);
#11083=ORIENTED_EDGE('',*,*,#8172,.F.);
#11084=ORIENTED_EDGE('',*,*,#8173,.T.);
#11085=ORIENTED_EDGE('',*,*,#8171,.F.);
#11086=ORIENTED_EDGE('',*,*,#8173,.F.);
#11087=ORIENTED_EDGE('',*,*,#8116,.T.);
#11088=ORIENTED_EDGE('',*,*,#8174,.T.);
#11089=ORIENTED_EDGE('',*,*,#8175,.T.);
#11090=ORIENTED_EDGE('',*,*,#8174,.F.);
#11091=ORIENTED_EDGE('',*,*,#8176,.F.);
#11092=ORIENTED_EDGE('',*,*,#8177,.T.);
#11093=ORIENTED_EDGE('',*,*,#8175,.F.);
#11094=ORIENTED_EDGE('',*,*,#8177,.F.);
#11095=ORIENTED_EDGE('',*,*,#8178,.T.);
#11096=ORIENTED_EDGE('',*,*,#8179,.T.);
#11097=ORIENTED_EDGE('',*,*,#8180,.T.);
#11098=ORIENTED_EDGE('',*,*,#8179,.F.);
#11099=ORIENTED_EDGE('',*,*,#8181,.F.);
#11100=ORIENTED_EDGE('',*,*,#8182,.F.);
#11101=ORIENTED_EDGE('',*,*,#8183,.F.);
#11102=ORIENTED_EDGE('',*,*,#8184,.F.);
#11103=ORIENTED_EDGE('',*,*,#8185,.F.);
#11104=ORIENTED_EDGE('',*,*,#8186,.F.);
#11105=ORIENTED_EDGE('',*,*,#8187,.F.);
#11106=ORIENTED_EDGE('',*,*,#8188,.F.);
#11107=ORIENTED_EDGE('',*,*,#8189,.F.);
#11108=ORIENTED_EDGE('',*,*,#8178,.F.);
#11109=ORIENTED_EDGE('',*,*,#8180,.F.);
#11110=ORIENTED_EDGE('',*,*,#8190,.T.);
#11111=ORIENTED_EDGE('',*,*,#8165,.T.);
#11112=ORIENTED_EDGE('',*,*,#8190,.F.);
#11113=ORIENTED_EDGE('',*,*,#8185,.T.);
#11114=ORIENTED_EDGE('',*,*,#8191,.T.);
#11115=ORIENTED_EDGE('',*,*,#8192,.T.);
#11116=ORIENTED_EDGE('',*,*,#8191,.F.);
#11117=ORIENTED_EDGE('',*,*,#8192,.F.);
#11118=ORIENTED_EDGE('',*,*,#8193,.T.);
#11119=ORIENTED_EDGE('',*,*,#8157,.T.);
#11120=ORIENTED_EDGE('',*,*,#8193,.F.);
#11121=ORIENTED_EDGE('',*,*,#8189,.T.);
#11122=ORIENTED_EDGE('',*,*,#8194,.T.);
#11123=ORIENTED_EDGE('',*,*,#8137,.T.);
#11124=ORIENTED_EDGE('',*,*,#8194,.F.);
#11125=ORIENTED_EDGE('',*,*,#8125,.T.);
#11126=ORIENTED_EDGE('',*,*,#8025,.T.);
#11127=ORIENTED_EDGE('',*,*,#8032,.T.);
#11128=ORIENTED_EDGE('',*,*,#8195,.T.);
#11129=ORIENTED_EDGE('',*,*,#8181,.T.);
#11130=ORIENTED_EDGE('',*,*,#8196,.T.);
#11131=ORIENTED_EDGE('',*,*,#8195,.F.);
#11132=ORIENTED_EDGE('',*,*,#8031,.T.);
#11133=ORIENTED_EDGE('',*,*,#8120,.T.);
#11134=ORIENTED_EDGE('',*,*,#8089,.T.);
#11135=ORIENTED_EDGE('',*,*,#8197,.F.);
#11136=ORIENTED_EDGE('',*,*,#8182,.T.);
#11137=ORIENTED_EDGE('',*,*,#8088,.T.);
#11138=ORIENTED_EDGE('',*,*,#8072,.T.);
#11139=ORIENTED_EDGE('',*,*,#8077,.T.);
#11140=ORIENTED_EDGE('',*,*,#8198,.T.);
#11141=ORIENTED_EDGE('',*,*,#8183,.T.);
#11142=ORIENTED_EDGE('',*,*,#8197,.T.);
#11143=ORIENTED_EDGE('',*,*,#8196,.F.);
#11144=ORIENTED_EDGE('',*,*,#8184,.T.);
#11145=ORIENTED_EDGE('',*,*,#8198,.F.);
#11146=ORIENTED_EDGE('',*,*,#8076,.T.);
#11147=ORIENTED_EDGE('',*,*,#8124,.T.);
#11148=ORIENTED_EDGE('',*,*,#8126,.T.);
#11149=ORIENTED_EDGE('',*,*,#8186,.T.);
#11150=ORIENTED_EDGE('',*,*,#8199,.T.);
#11151=ORIENTED_EDGE('',*,*,#8176,.T.);
#11152=ORIENTED_EDGE('',*,*,#8199,.F.);
#11153=ORIENTED_EDGE('',*,*,#8188,.T.);
#11154=ORIENTED_EDGE('',*,*,#8200,.T.);
#11155=ORIENTED_EDGE('',*,*,#8172,.T.);
#11156=ORIENTED_EDGE('',*,*,#8200,.F.);
#11157=ORIENTED_EDGE('',*,*,#8187,.T.);
#11158=ORIENTED_EDGE('',*,*,#8201,.T.);
#11159=ORIENTED_EDGE('',*,*,#8168,.T.);
#11160=ORIENTED_EDGE('',*,*,#8201,.F.);
#11161=ORIENTED_EDGE('',*,*,#8041,.F.);
#11162=ORIENTED_EDGE('',*,*,#8078,.T.);
#11163=ORIENTED_EDGE('',*,*,#8068,.F.);
#11164=ORIENTED_EDGE('',*,*,#8050,.T.);
#11165=ORIENTED_EDGE('',*,*,#7999,.F.);
#11166=ORIENTED_EDGE('',*,*,#8009,.T.);
#11167=ORIENTED_EDGE('',*,*,#8102,.F.);
#11168=ORIENTED_EDGE('',*,*,#8027,.T.);
#11169=ORIENTED_EDGE('',*,*,#8015,.F.);
#11170=ORIENTED_EDGE('',*,*,#8127,.T.);
#11171=ORIENTED_EDGE('',*,*,#8045,.F.);
#11172=ORIENTED_EDGE('',*,*,#8018,.T.);
#14898=PLANE('',#16650);
#14899=PLANE('',#16651);
#14900=PLANE('',#16652);
#14901=PLANE('',#16653);
#14902=PLANE('',#16654);
#14903=PLANE('',#16655);
#14904=PLANE('',#16656);
#14905=PLANE('',#16657);
#14906=PLANE('',#16658);
#14907=PLANE('',#16659);
#14908=PLANE('',#16660);
#14909=PLANE('',#16661);
#14910=PLANE('',#16662);
#14911=PLANE('',#16663);
#14912=PLANE('',#16664);
#14913=PLANE('',#16665);
#14914=PLANE('',#16666);
#14915=PLANE('',#16667);
#14916=PLANE('',#16668);
#14917=PLANE('',#16669);
#14918=PLANE('',#16670);
#14919=PLANE('',#16671);
#14920=PLANE('',#16672);
#14921=PLANE('',#16673);
#14922=PLANE('',#16674);
#14923=PLANE('',#16675);
#14924=PLANE('',#16676);
#14925=PLANE('',#16677);
#14926=PLANE('',#16678);
#14927=PLANE('',#16679);
#14928=PLANE('',#16680);
#14929=PLANE('',#16681);
#14930=PLANE('',#16682);
#14931=PLANE('',#16683);
#14932=PLANE('',#16684);
#14933=PLANE('',#16691);
#14934=PLANE('',#16692);
#14935=PLANE('',#16693);
#14936=PLANE('',#16694);
#14937=PLANE('',#16695);
#14938=PLANE('',#16708);
#14939=PLANE('',#16714);
#14940=PLANE('',#16727);
#14941=PLANE('',#16736);
#14942=PLANE('',#16753);
#14943=PLANE('',#16764);
#14944=PLANE('',#16765);
#14945=PLANE('',#16766);
#14946=PLANE('',#16767);
#14947=PLANE('',#16771);
#14948=PLANE('',#16772);
#14949=PLANE('',#16773);
#15473=ADVANCED_FACE('',(#1930),#14898,.T.);
#15474=ADVANCED_FACE('',(#1931),#14899,.T.);
#15475=ADVANCED_FACE('',(#1932),#14900,.T.);
#15476=ADVANCED_FACE('',(#1933),#14901,.T.);
#15477=ADVANCED_FACE('',(#1934),#14902,.T.);
#15478=ADVANCED_FACE('',(#1935),#14903,.T.);
#15479=ADVANCED_FACE('',(#1936),#14904,.T.);
#15480=ADVANCED_FACE('',(#1937),#14905,.T.);
#15481=ADVANCED_FACE('',(#1938),#14906,.T.);
#15482=ADVANCED_FACE('',(#1939),#14907,.T.);
#15483=ADVANCED_FACE('',(#1940),#14908,.T.);
#15484=ADVANCED_FACE('',(#1941),#14909,.T.);
#15485=ADVANCED_FACE('',(#1942),#14910,.T.);
#15486=ADVANCED_FACE('',(#1943),#14911,.T.);
#15487=ADVANCED_FACE('',(#1944),#14912,.T.);
#15488=ADVANCED_FACE('',(#1945),#14913,.T.);
#15489=ADVANCED_FACE('',(#1946),#14914,.T.);
#15490=ADVANCED_FACE('',(#1947),#14915,.T.);
#15491=ADVANCED_FACE('',(#1948),#14916,.T.);
#15492=ADVANCED_FACE('',(#1949),#14917,.T.);
#15493=ADVANCED_FACE('',(#1950),#14918,.T.);
#15494=ADVANCED_FACE('',(#1951),#14919,.T.);
#15495=ADVANCED_FACE('',(#1952),#14920,.T.);
#15496=ADVANCED_FACE('',(#1953),#14921,.T.);
#15497=ADVANCED_FACE('',(#1954),#14922,.T.);
#15498=ADVANCED_FACE('',(#1955),#14923,.T.);
#15499=ADVANCED_FACE('',(#1956),#14924,.T.);
#15500=ADVANCED_FACE('',(#1957),#14925,.T.);
#15501=ADVANCED_FACE('',(#1958),#14926,.T.);
#15502=ADVANCED_FACE('',(#1959),#14927,.T.);
#15503=ADVANCED_FACE('',(#1960),#14928,.T.);
#15504=ADVANCED_FACE('',(#1961),#14929,.T.);
#15505=ADVANCED_FACE('',(#1962),#14930,.T.);
#15506=ADVANCED_FACE('',(#1963),#14931,.T.);
#15507=ADVANCED_FACE('',(#1964,#1169,#1170,#1171,#1172,#1173,#1174),#14932,
 .T.);
#15508=ADVANCED_FACE('',(#1965),#14933,.T.);
#15509=ADVANCED_FACE('',(#1966),#14934,.T.);
#15510=ADVANCED_FACE('',(#1967),#14935,.T.);
#15511=ADVANCED_FACE('',(#1968),#14936,.T.);
#15512=ADVANCED_FACE('',(#1969),#14937,.T.);
#15513=ADVANCED_FACE('',(#1970),#1715,.F.);
#15514=ADVANCED_FACE('',(#1971),#896,.F.);
#15515=ADVANCED_FACE('',(#1972),#1716,.F.);
#15516=ADVANCED_FACE('',(#1973),#1717,.F.);
#15517=ADVANCED_FACE('',(#1974,#1175),#14938,.F.);
#15518=ADVANCED_FACE('',(#1975),#1718,.F.);
#15519=ADVANCED_FACE('',(#1976,#1176),#14939,.F.);
#15520=ADVANCED_FACE('',(#1977),#897,.F.);
#15521=ADVANCED_FACE('',(#1978),#1719,.F.);
#15522=ADVANCED_FACE('',(#1979),#898,.F.);
#15523=ADVANCED_FACE('',(#1980),#1720,.F.);
#15524=ADVANCED_FACE('',(#1981),#899,.F.);
#15525=ADVANCED_FACE('',(#1982),#1721,.F.);
#15526=ADVANCED_FACE('',(#1983,#1177),#14940,.F.);
#15527=ADVANCED_FACE('',(#1984),#1722,.F.);
#15528=ADVANCED_FACE('',(#1985),#900,.F.);
#15529=ADVANCED_FACE('',(#1986),#1723,.F.);
#15530=ADVANCED_FACE('',(#1987,#1178),#14941,.F.);
#15531=ADVANCED_FACE('',(#1988),#1724,.F.);
#15532=ADVANCED_FACE('',(#1989),#901,.F.);
#15533=ADVANCED_FACE('',(#1990),#1725,.F.);
#15534=ADVANCED_FACE('',(#1991),#902,.F.);
#15535=ADVANCED_FACE('',(#1992),#1726,.F.);
#15536=ADVANCED_FACE('',(#1993),#903,.F.);
#15537=ADVANCED_FACE('',(#1994),#1727,.F.);
#15538=ADVANCED_FACE('',(#1995,#1179,#1180,#1181,#1182,#1183,#1184),#14942,
 .F.);
#15539=ADVANCED_FACE('',(#1996),#904,.F.);
#15540=ADVANCED_FACE('',(#1997),#1728,.F.);
#15541=ADVANCED_FACE('',(#1998),#905,.F.);
#15542=ADVANCED_FACE('',(#1999),#1729,.F.);
#15543=ADVANCED_FACE('',(#2000),#14943,.T.);
#15544=ADVANCED_FACE('',(#2001),#14944,.T.);
#15545=ADVANCED_FACE('',(#2002),#14945,.T.);
#15546=ADVANCED_FACE('',(#2003),#14946,.T.);
#15547=ADVANCED_FACE('',(#2004),#1730,.F.);
#15548=ADVANCED_FACE('',(#2005),#1731,.F.);
#15549=ADVANCED_FACE('',(#2006),#1732,.F.);
#15550=ADVANCED_FACE('',(#2007),#14947,.T.);
#15551=ADVANCED_FACE('',(#2008),#14948,.T.);
#15552=ADVANCED_FACE('',(#2009),#14949,.T.);
#16237=CLOSED_SHELL('',(#15473,#15474,#15475,#15476,#15477,#15478,#15479,
#15480,#15481,#15482,#15483,#15484,#15485,#15486,#15487,#15488,#15489,#15490,
#15491,#15492,#15493,#15494,#15495,#15496,#15497,#15498,#15499,#15500,#15501,
#15502,#15503,#15504,#15505,#15506,#15507,#15508,#15509,#15510,#15511,#15512,
#15513,#15514,#15515,#15516,#15517,#15518,#15519,#15520,#15521,#15522,#15523,
#15524,#15525,#15526,#15527,#15528,#15529,#15530,#15531,#15532,#15533,#15534,
#15535,#15536,#15537,#15538,#15539,#15540,#15541,#15542,#15543,#15544,#15545,
#15546,#15547,#15548,#15549,#15550,#15551,#15552));
#16649=AXIS2_PLACEMENT_3D('',#22961,#18558,#18559);
#16650=AXIS2_PLACEMENT_3D('',#22962,#18560,#18561);
#16651=AXIS2_PLACEMENT_3D('',#22975,#18568,#18569);
#16652=AXIS2_PLACEMENT_3D('',#22985,#18575,#18576);
#16653=AXIS2_PLACEMENT_3D('',#22999,#18584,#18585);
#16654=AXIS2_PLACEMENT_3D('',#23003,#18588,#18589);
#16655=AXIS2_PLACEMENT_3D('',#23013,#18595,#18596);
#16656=AXIS2_PLACEMENT_3D('',#23015,#18598,#18599);
#16657=AXIS2_PLACEMENT_3D('',#23027,#18606,#18607);
#16658=AXIS2_PLACEMENT_3D('',#23033,#18611,#18612);
#16659=AXIS2_PLACEMENT_3D('',#23045,#18619,#18620);
#16660=AXIS2_PLACEMENT_3D('',#23055,#18626,#18627);
#16661=AXIS2_PLACEMENT_3D('',#23065,#18633,#18634);
#16662=AXIS2_PLACEMENT_3D('',#23069,#18637,#18638);
#16663=AXIS2_PLACEMENT_3D('',#23075,#18642,#18643);
#16664=AXIS2_PLACEMENT_3D('',#23079,#18646,#18647);
#16665=AXIS2_PLACEMENT_3D('',#23091,#18654,#18655);
#16666=AXIS2_PLACEMENT_3D('',#23101,#18661,#18662);
#16667=AXIS2_PLACEMENT_3D('',#23111,#18668,#18669);
#16668=AXIS2_PLACEMENT_3D('',#23115,#18672,#18673);
#16669=AXIS2_PLACEMENT_3D('',#23121,#18677,#18678);
#16670=AXIS2_PLACEMENT_3D('',#23127,#18682,#18683);
#16671=AXIS2_PLACEMENT_3D('',#23136,#18689,#18690);
#16672=AXIS2_PLACEMENT_3D('',#23150,#18698,#18699);
#16673=AXIS2_PLACEMENT_3D('',#23154,#18702,#18703);
#16674=AXIS2_PLACEMENT_3D('',#23164,#18709,#18710);
#16675=AXIS2_PLACEMENT_3D('',#23171,#18715,#18716);
#16676=AXIS2_PLACEMENT_3D('',#23175,#18719,#18720);
#16677=AXIS2_PLACEMENT_3D('',#23177,#18722,#18723);
#16678=AXIS2_PLACEMENT_3D('',#23182,#18727,#18728);
#16679=AXIS2_PLACEMENT_3D('',#23185,#18731,#18732);
#16680=AXIS2_PLACEMENT_3D('',#23186,#18733,#18734);
#16681=AXIS2_PLACEMENT_3D('',#23193,#18739,#18740);
#16682=AXIS2_PLACEMENT_3D('',#23197,#18743,#18744);
#16683=AXIS2_PLACEMENT_3D('',#23198,#18745,#18746);
#16684=AXIS2_PLACEMENT_3D('',#23202,#18749,#18750);
#16685=AXIS2_PLACEMENT_3D('',#23205,#18752,#18753);
#16686=AXIS2_PLACEMENT_3D('',#23207,#18754,#18755);
#16687=AXIS2_PLACEMENT_3D('',#23209,#18756,#18757);
#16688=AXIS2_PLACEMENT_3D('',#23211,#18758,#18759);
#16689=AXIS2_PLACEMENT_3D('',#23213,#18760,#18761);
#16690=AXIS2_PLACEMENT_3D('',#23215,#18762,#18763);
#16691=AXIS2_PLACEMENT_3D('',#23216,#18764,#18765);
#16692=AXIS2_PLACEMENT_3D('',#23217,#18766,#18767);
#16693=AXIS2_PLACEMENT_3D('',#23219,#18769,#18770);
#16694=AXIS2_PLACEMENT_3D('',#23223,#18773,#18774);
#16695=AXIS2_PLACEMENT_3D('',#23227,#18777,#18778);
#16696=AXIS2_PLACEMENT_3D('',#23232,#18782,#18783);
#16697=AXIS2_PLACEMENT_3D('',#23235,#18784,#18785);
#16698=AXIS2_PLACEMENT_3D('',#23236,#18786,#18787);
#16699=AXIS2_PLACEMENT_3D('',#23240,#18789,#18790);
#16700=AXIS2_PLACEMENT_3D('',#23241,#18791,#18792);
#16701=AXIS2_PLACEMENT_3D('',#23242,#18793,#18794);
#16702=AXIS2_PLACEMENT_3D('',#23245,#18795,#18796);
#16703=AXIS2_PLACEMENT_3D('',#23246,#18797,#18798);
#16704=AXIS2_PLACEMENT_3D('',#23248,#18800,#18801);
#16705=AXIS2_PLACEMENT_3D('',#23251,#18803,#18804);
#16706=AXIS2_PLACEMENT_3D('',#23252,#18805,#18806);
#16707=AXIS2_PLACEMENT_3D('',#23254,#18807,#18808);
#16708=AXIS2_PLACEMENT_3D('',#23256,#18810,#18811);
#16709=AXIS2_PLACEMENT_3D('',#23258,#18812,#18813);
#16710=AXIS2_PLACEMENT_3D('',#23259,#18814,#18815);
#16711=AXIS2_PLACEMENT_3D('',#23261,#18816,#18817);
#16712=AXIS2_PLACEMENT_3D('',#23265,#18819,#18820);
#16713=AXIS2_PLACEMENT_3D('',#23266,#18821,#18822);
#16714=AXIS2_PLACEMENT_3D('',#23267,#18823,#18824);
#16715=AXIS2_PLACEMENT_3D('',#23269,#18825,#18826);
#16716=AXIS2_PLACEMENT_3D('',#23270,#18827,#18828);
#16717=AXIS2_PLACEMENT_3D('',#23272,#18830,#18831);
#16718=AXIS2_PLACEMENT_3D('',#23275,#18833,#18834);
#16719=AXIS2_PLACEMENT_3D('',#23276,#18835,#18836);
#16720=AXIS2_PLACEMENT_3D('',#23278,#18838,#18839);
#16721=AXIS2_PLACEMENT_3D('',#23281,#18841,#18842);
#16722=AXIS2_PLACEMENT_3D('',#23282,#18843,#18844);
#16723=AXIS2_PLACEMENT_3D('',#23285,#18845,#18846);
#16724=AXIS2_PLACEMENT_3D('',#23286,#18847,#18848);
#16725=AXIS2_PLACEMENT_3D('',#23288,#18850,#18851);
#16726=AXIS2_PLACEMENT_3D('',#23290,#18852,#18853);
#16727=AXIS2_PLACEMENT_3D('',#23292,#18855,#18856);
#16728=AXIS2_PLACEMENT_3D('',#23294,#18857,#18858);
#16729=AXIS2_PLACEMENT_3D('',#23295,#18859,#18860);
#16730=AXIS2_PLACEMENT_3D('',#23298,#18862,#18863);
#16731=AXIS2_PLACEMENT_3D('',#23299,#18864,#18865);
#16732=AXIS2_PLACEMENT_3D('',#23302,#18866,#18867);
#16733=AXIS2_PLACEMENT_3D('',#23303,#18868,#18869);
#16734=AXIS2_PLACEMENT_3D('',#23305,#18871,#18872);
#16735=AXIS2_PLACEMENT_3D('',#23307,#18873,#18874);
#16736=AXIS2_PLACEMENT_3D('',#23309,#18876,#18877);
#16737=AXIS2_PLACEMENT_3D('',#23311,#18878,#18879);
#16738=AXIS2_PLACEMENT_3D('',#23312,#18880,#18881);
#16739=AXIS2_PLACEMENT_3D('',#23315,#18883,#18884);
#16740=AXIS2_PLACEMENT_3D('',#23316,#18885,#18886);
#16741=AXIS2_PLACEMENT_3D('',#23318,#18887,#18888);
#16742=AXIS2_PLACEMENT_3D('',#23320,#18890,#18891);
#16743=AXIS2_PLACEMENT_3D('',#23323,#18893,#18894);
#16744=AXIS2_PLACEMENT_3D('',#23324,#18895,#18896);
#16745=AXIS2_PLACEMENT_3D('',#23326,#18897,#18898);
#16746=AXIS2_PLACEMENT_3D('',#23328,#18900,#18901);
#16747=AXIS2_PLACEMENT_3D('',#23331,#18903,#18904);
#16748=AXIS2_PLACEMENT_3D('',#23332,#18905,#18906);
#16749=AXIS2_PLACEMENT_3D('',#23334,#18907,#18908);
#16750=AXIS2_PLACEMENT_3D('',#23336,#18910,#18911);
#16751=AXIS2_PLACEMENT_3D('',#23338,#18912,#18913);
#16752=AXIS2_PLACEMENT_3D('',#23341,#18915,#18916);
#16753=AXIS2_PLACEMENT_3D('',#23342,#18917,#18918);
#16754=AXIS2_PLACEMENT_3D('',#23352,#18923,#18924);
#16755=AXIS2_PLACEMENT_3D('',#23354,#18925,#18926);
#16756=AXIS2_PLACEMENT_3D('',#23356,#18927,#18928);
#16757=AXIS2_PLACEMENT_3D('',#23358,#18929,#18930);
#16758=AXIS2_PLACEMENT_3D('',#23360,#18931,#18932);
#16759=AXIS2_PLACEMENT_3D('',#23361,#18933,#18934);
#16760=AXIS2_PLACEMENT_3D('',#23363,#18936,#18937);
#16761=AXIS2_PLACEMENT_3D('',#23366,#18939,#18940);
#16762=AXIS2_PLACEMENT_3D('',#23367,#18941,#18942);
#16763=AXIS2_PLACEMENT_3D('',#23369,#18944,#18945);
#16764=AXIS2_PLACEMENT_3D('',#23371,#18947,#18948);
#16765=AXIS2_PLACEMENT_3D('',#23374,#18951,#18952);
#16766=AXIS2_PLACEMENT_3D('',#23376,#18954,#18955);
#16767=AXIS2_PLACEMENT_3D('',#23378,#18957,#18958);
#16768=AXIS2_PLACEMENT_3D('',#23379,#18959,#18960);
#16769=AXIS2_PLACEMENT_3D('',#23381,#18962,#18963);
#16770=AXIS2_PLACEMENT_3D('',#23383,#18965,#18966);
#16771=AXIS2_PLACEMENT_3D('',#23385,#18968,#18969);
#16772=AXIS2_PLACEMENT_3D('',#23386,#18970,#18971);
#16773=AXIS2_PLACEMENT_3D('',#23387,#18972,#18973);
#18558=DIRECTION('axis',(0.,0.,1.));
#18559=DIRECTION('refdir',(1.,0.,0.));
#18560=DIRECTION('center_axis',(0.923879532511287,0.382683432365089,0.));
#18561=DIRECTION('ref_axis',(0.,0.,-1.));
#18562=DIRECTION('',(-0.336556770590777,0.812519920068747,0.475963149477966));
#18563=DIRECTION('',(0.,0.,1.));
#18564=DIRECTION('',(0.336556770590775,-0.812519920068743,0.475963149477973));
#18565=DIRECTION('',(0.28108463771482,-0.678598344545848,-0.678598344545846));
#18566=DIRECTION('',(0.,0.,-1.));
#18567=DIRECTION('',(-0.281084637714818,0.678598344545843,-0.678598344545852));
#18568=DIRECTION('center_axis',(0.923879532511287,0.,0.38268343236509));
#18569=DIRECTION('ref_axis',(0.38268343236509,0.,-0.923879532511287));
#18570=DIRECTION('',(-0.33655677059078,-0.475963149477958,0.81251992006875));
#18571=DIRECTION('',(0.,-1.,0.));
#18572=DIRECTION('',(0.33655677059078,-0.475963149477958,-0.81251992006875));
#18573=DIRECTION('',(0.357406744336593,0.357406744336595,-0.862856209461016));
#18574=DIRECTION('',(0.,1.,0.));
#18575=DIRECTION('center_axis',(0.57735026918963,0.577350269189628,0.57735026918962));
#18576=DIRECTION('ref_axis',(0.707106781186541,0.,-0.707106781186554));
#18577=DIRECTION('',(0.707106781186546,-0.707106781186549,0.));
#18578=DIRECTION('',(0.812519920068742,-0.336556770590782,-0.47596314947797));
#18579=DIRECTION('',(0.475963149477956,0.336556770590781,-0.812519920068751));
#18580=DIRECTION('',(0.,0.707106781186543,-0.707106781186552));
#18581=DIRECTION('',(-0.475963149477964,0.812519920068745,-0.336556770590783));
#18582=DIRECTION('',(-0.81251992006874,0.475963149477997,0.336556770590751));
#18583=DIRECTION('',(-0.707106781186541,0.,0.707106781186554));
#18584=DIRECTION('center_axis',(0.707106781186549,0.707106781186546,0.));
#18585=DIRECTION('ref_axis',(0.,0.,-1.));
#18586=DIRECTION('',(-0.707106781186546,0.707106781186549,0.));
#18587=DIRECTION('',(0.,0.,-1.));
#18588=DIRECTION('center_axis',(0.923879532511289,0.,-0.382683432365084));
#18589=DIRECTION('ref_axis',(-0.382683432365084,0.,-0.923879532511289));
#18590=DIRECTION('',(0.,-1.,0.));
#18591=DIRECTION('',(-0.357406744336588,-0.35740674433659,-0.86285620946102));
#18592=DIRECTION('',(-0.336556770590771,0.475963149477975,-0.812519920068744));
#18593=DIRECTION('',(0.,1.,0.));
#18594=DIRECTION('',(0.336556770590771,0.475963149477975,0.812519920068744));
#18595=DIRECTION('center_axis',(1.,0.,0.));
#18596=DIRECTION('ref_axis',(0.,0.,-1.));
#18597=DIRECTION('',(0.,0.,1.));
#18598=DIRECTION('center_axis',(0.577350269189627,0.577350269189624,-0.577350269189627));
#18599=DIRECTION('ref_axis',(-0.707106781186548,0.,-0.707106781186548));
#18600=DIRECTION('',(0.707106781186548,0.,0.707106781186548));
#18601=DIRECTION('',(0.812519920068745,-0.475963149477963,0.336556770590785));
#18602=DIRECTION('',(0.475963149477962,-0.812519920068747,-0.336556770590781));
#18603=DIRECTION('',(0.,-0.707106781186549,-0.707106781186546));
#18604=DIRECTION('',(-0.475963149477966,-0.336556770590781,-0.812519920068745));
#18605=DIRECTION('',(-0.812519920068746,0.336556770590784,-0.475963149477963));
#18606=DIRECTION('center_axis',(0.707106781186549,-0.707106781186546,0.));
#18607=DIRECTION('ref_axis',(0.,0.,-1.));
#18608=DIRECTION('',(-0.707106781186546,-0.707106781186549,0.));
#18609=DIRECTION('',(0.,0.,1.));
#18610=DIRECTION('',(0.707106781186546,0.707106781186549,0.));
#18611=DIRECTION('center_axis',(0.57735026918963,-0.577350269189628,0.57735026918962));
#18612=DIRECTION('ref_axis',(0.707106781186541,0.,-0.707106781186554));
#18613=DIRECTION('',(0.707106781186541,0.,-0.707106781186554));
#18614=DIRECTION('',(0.81251992006874,0.475963149477997,-0.336556770590751));
#18615=DIRECTION('',(0.475963149477962,0.812519920068746,0.336556770590786));
#18616=DIRECTION('',(0.,0.707106781186543,0.707106781186552));
#18617=DIRECTION('',(-0.475963149477956,0.336556770590782,0.812519920068751));
#18618=DIRECTION('',(-0.812519920068742,-0.336556770590782,0.475963149477971));
#18619=DIRECTION('center_axis',(0.,0.382683432365093,-0.923879532511286));
#18620=DIRECTION('ref_axis',(-1.,0.,0.));
#18621=DIRECTION('',(0.475963149477956,0.81251992006875,0.336556770590782));
#18622=DIRECTION('',(1.,0.,0.));
#18623=DIRECTION('',(-0.678598344545842,-0.67859834454585,-0.281084637714824));
#18624=DIRECTION('',(-1.,0.,0.));
#18625=DIRECTION('',(-0.678598344545842,0.67859834454585,0.281084637714824));
#18626=DIRECTION('center_axis',(-0.382683432365097,0.,-0.923879532511284));
#18627=DIRECTION('ref_axis',(-0.923879532511284,0.,0.382683432365097));
#18628=DIRECTION('',(0.,-1.,0.));
#18629=DIRECTION('',(-0.678598344545841,-0.678598344545852,0.281084637714824));
#18630=DIRECTION('',(-0.81251992006874,0.475963149477974,0.336556770590782));
#18631=DIRECTION('',(0.,1.,0.));
#18632=DIRECTION('',(0.81251992006874,0.475963149477974,-0.336556770590782));
#18633=DIRECTION('center_axis',(0.,0.,-1.));
#18634=DIRECTION('ref_axis',(-1.,0.,0.));
#18635=DIRECTION('',(0.,1.,0.));
#18636=DIRECTION('',(1.,0.,0.));
#18637=DIRECTION('center_axis',(0.382683432365097,0.,-0.923879532511284));
#18638=DIRECTION('ref_axis',(-0.923879532511284,0.,-0.382683432365097));
#18639=DIRECTION('',(0.,-1.,0.));
#18640=DIRECTION('',(-0.812519920068745,-0.475963149477963,-0.336556770590785));
#18641=DIRECTION('',(-0.678598344545841,0.678598344545852,-0.281084637714824));
#18642=DIRECTION('center_axis',(0.,0.707106781186546,-0.707106781186549));
#18643=DIRECTION('ref_axis',(-1.,0.,0.));
#18644=DIRECTION('',(0.,0.707106781186549,0.707106781186546));
#18645=DIRECTION('',(-1.,0.,0.));
#18646=DIRECTION('center_axis',(-0.577350269189634,0.577350269189621,-0.577350269189623));
#18647=DIRECTION('ref_axis',(-0.707106781186541,0.,0.707106781186554));
#18648=DIRECTION('',(0.707106781186541,0.,-0.707106781186554));
#18649=DIRECTION('',(0.336556770590786,-0.475963149477958,-0.812519920068748));
#18650=DIRECTION('',(-0.336556770590778,-0.812519920068749,-0.475963149477962));
#18651=DIRECTION('',(-0.707106781186546,-0.707106781186549,1.25607396694702E-14));
#18652=DIRECTION('',(-0.81251992006874,-0.336556770590781,0.475963149477975));
#18653=DIRECTION('',(-0.475963149477959,0.336556770590782,0.812519920068749));
#18654=DIRECTION('center_axis',(-0.923879532511287,0.382683432365089,0.));
#18655=DIRECTION('ref_axis',(0.,0.,1.));
#18656=DIRECTION('',(0.336556770590775,0.812519920068743,-0.475963149477973));
#18657=DIRECTION('',(0.,0.,-1.));
#18658=DIRECTION('',(-0.281084637714823,-0.678598344545855,0.678598344545838));
#18659=DIRECTION('',(0.,0.,1.));
#18660=DIRECTION('',(0.28108463771483,0.678598344545872,0.678598344545818));
#18661=DIRECTION('center_axis',(-0.923879532511276,0.,0.382683432365115));
#18662=DIRECTION('ref_axis',(0.382683432365115,0.,0.923879532511276));
#18663=DIRECTION('',(0.,-1.,0.));
#18664=DIRECTION('',(0.357406744336614,-0.357406744336615,0.862856209460999));
#18665=DIRECTION('',(0.336556770590807,0.475963149477934,0.812519920068753));
#18666=DIRECTION('',(0.,1.,0.));
#18667=DIRECTION('',(-0.336556770590807,0.475963149477934,-0.812519920068753));
#18668=DIRECTION('center_axis',(-1.,0.,0.));
#18669=DIRECTION('ref_axis',(0.,0.,1.));
#18670=DIRECTION('',(0.,1.,0.));
#18671=DIRECTION('',(0.,0.,-1.));
#18672=DIRECTION('center_axis',(-0.923879532511284,0.,-0.382683432365097));
#18673=DIRECTION('ref_axis',(-0.382683432365097,0.,0.923879532511284));
#18674=DIRECTION('',(0.,-1.,0.));
#18675=DIRECTION('',(-0.336556770590786,-0.475963149477958,0.812519920068748));
#18676=DIRECTION('',(-0.357406744336599,0.3574067443366,0.862856209461012));
#18677=DIRECTION('center_axis',(-0.707106781186549,-0.707106781186546,0.));
#18678=DIRECTION('ref_axis',(0.,0.,1.));
#18679=DIRECTION('',(0.707106781186546,-0.707106781186549,-1.25607396694702E-14));
#18680=DIRECTION('',(0.,0.,-1.));
#18681=DIRECTION('',(-0.707106781186546,0.707106781186549,0.));
#18682=DIRECTION('center_axis',(-0.577350269189634,-0.577350269189621,-0.577350269189623));
#18683=DIRECTION('ref_axis',(-0.707106781186541,0.,0.707106781186554));
#18684=DIRECTION('',(-0.475963149477957,0.81251992006875,-0.336556770590781));
#18685=DIRECTION('',(0.,0.707106781186549,-0.707106781186546));
#18686=DIRECTION('',(0.475963149477953,0.33655677059079,-0.812519920068749));
#18687=DIRECTION('',(0.81251992006874,-0.336556770590781,-0.475963149477975));
#18688=DIRECTION('',(-0.707106781186541,0.,0.707106781186554));
#18689=DIRECTION('center_axis',(-0.57735026918963,0.577350269189628,0.57735026918962));
#18690=DIRECTION('ref_axis',(0.707106781186541,0.,0.707106781186554));
#18691=DIRECTION('',(-0.707106781186541,0.,-0.707106781186554));
#18692=DIRECTION('',(-0.81251992006874,-0.475963149477994,-0.336556770590754));
#18693=DIRECTION('',(-0.475963149477964,-0.812519920068745,0.336556770590783));
#18694=DIRECTION('',(0.,-0.707106781186543,0.707106781186552));
#18695=DIRECTION('',(0.475963149477957,-0.336556770590781,0.812519920068751));
#18696=DIRECTION('',(0.812519920068742,0.336556770590782,0.47596314947797));
#18697=DIRECTION('',(0.707106781186546,0.707106781186549,0.));
#18698=DIRECTION('center_axis',(-0.707106781186554,0.,0.707106781186541));
#18699=DIRECTION('ref_axis',(0.707106781186541,0.,0.707106781186554));
#18700=DIRECTION('',(0.707106781186541,0.,0.707106781186554));
#18701=DIRECTION('',(0.,-1.,0.));
#18702=DIRECTION('center_axis',(-0.57735026918963,-0.577350269189628,0.57735026918962));
#18703=DIRECTION('ref_axis',(0.707106781186541,0.,0.707106781186554));
#18704=DIRECTION('',(-0.812519920068742,0.336556770590782,-0.475963149477971));
#18705=DIRECTION('',(-0.475963149477956,-0.336556770590782,-0.812519920068751));
#18706=DIRECTION('',(0.,-0.707106781186543,-0.707106781186552));
#18707=DIRECTION('',(0.475963149477962,-0.812519920068746,-0.336556770590786));
#18708=DIRECTION('',(0.81251992006874,-0.475963149477994,0.336556770590754));
#18709=DIRECTION('center_axis',(0.,0.382683432365095,0.923879532511284));
#18710=DIRECTION('ref_axis',(1.,0.,0.));
#18711=DIRECTION('',(-1.,0.,0.));
#18712=DIRECTION('',(0.678598344545875,-0.678598344545821,0.281084637714814));
#18713=DIRECTION('',(1.,0.,0.));
#18714=DIRECTION('',(0.678598344545879,0.678598344545818,-0.281084637714813));
#18715=DIRECTION('center_axis',(-0.382683432365069,0.,0.923879532511295));
#18716=DIRECTION('ref_axis',(0.923879532511295,0.,0.382683432365069));
#18717=DIRECTION('',(0.678598344545878,0.678598344545818,0.281084637714815));
#18718=DIRECTION('',(0.,1.,0.));
#18719=DIRECTION('center_axis',(0.,0.707106781186552,0.707106781186543));
#18720=DIRECTION('ref_axis',(1.,0.,0.));
#18721=DIRECTION('',(1.,0.,0.));
#18722=DIRECTION('center_axis',(0.382683432365067,0.,0.923879532511296));
#18723=DIRECTION('ref_axis',(0.923879532511296,0.,-0.382683432365067));
#18724=DIRECTION('',(0.,-1.,0.));
#18725=DIRECTION('',(0.678598344545881,-0.678598344545815,-0.281084637714814));
#18726=DIRECTION('',(0.,1.,0.));
#18727=DIRECTION('center_axis',(0.,-0.382683432365098,0.923879532511283));
#18728=DIRECTION('ref_axis',(1.,0.,0.));
#18729=DIRECTION('',(-1.,0.,0.));
#18730=DIRECTION('',(1.,0.,0.));
#18731=DIRECTION('center_axis',(0.,0.,1.));
#18732=DIRECTION('ref_axis',(1.,0.,0.));
#18733=DIRECTION('center_axis',(-0.382683432365096,0.923879532511284,0.));
#18734=DIRECTION('ref_axis',(0.,0.,1.));
#18735=DIRECTION('',(0.,0.,1.));
#18736=DIRECTION('',(0.678598344545842,0.281084637714823,-0.678598344545851));
#18737=DIRECTION('',(0.,0.,-1.));
#18738=DIRECTION('',(-0.678598344545843,-0.281084637714824,-0.678598344545849));
#18739=DIRECTION('center_axis',(0.,0.923879532511286,0.382683432365091));
#18740=DIRECTION('ref_axis',(0.,-0.382683432365091,0.923879532511286));
#18741=DIRECTION('',(0.678598344545842,-0.281084637714823,0.678598344545851));
#18742=DIRECTION('',(-1.,0.,0.));
#18743=DIRECTION('center_axis',(-0.707106781186549,0.707106781186546,0.));
#18744=DIRECTION('ref_axis',(0.,0.,1.));
#18745=DIRECTION('center_axis',(0.382683432365096,0.923879532511284,0.));
#18746=DIRECTION('ref_axis',(0.,0.,1.));
#18747=DIRECTION('',(-0.678598344545843,0.281084637714824,0.678598344545849));
#18748=DIRECTION('',(0.,0.,1.));
#18749=DIRECTION('center_axis',(0.,1.,0.));
#18750=DIRECTION('ref_axis',(0.,0.,1.));
#18751=DIRECTION('',(1.,0.,0.));
#18752=DIRECTION('center_axis',(0.,1.,0.));
#18753=DIRECTION('ref_axis',(0.,0.,1.));
#18754=DIRECTION('center_axis',(0.,1.,0.));
#18755=DIRECTION('ref_axis',(0.,0.,1.));
#18756=DIRECTION('center_axis',(0.,1.,0.));
#18757=DIRECTION('ref_axis',(0.,0.,1.));
#18758=DIRECTION('center_axis',(0.,1.,0.));
#18759=DIRECTION('ref_axis',(0.,0.,1.));
#18760=DIRECTION('center_axis',(0.,1.,0.));
#18761=DIRECTION('ref_axis',(0.,0.,1.));
#18762=DIRECTION('center_axis',(0.,1.,0.));
#18763=DIRECTION('ref_axis',(1.,0.,0.));
#18764=DIRECTION('center_axis',(0.,0.923879532511285,-0.382683432365093));
#18765=DIRECTION('ref_axis',(0.,0.382683432365093,0.923879532511285));
#18766=DIRECTION('center_axis',(0.,-0.707106781186552,0.707106781186543));
#18767=DIRECTION('ref_axis',(1.,0.,0.));
#18768=DIRECTION('',(-1.,0.,0.));
#18769=DIRECTION('center_axis',(0.,-0.382683432365092,-0.923879532511286));
#18770=DIRECTION('ref_axis',(-1.,0.,0.));
#18771=DIRECTION('',(-0.475963149477963,-0.812519920068747,0.33655677059078));
#18772=DIRECTION('',(-1.,0.,0.));
#18773=DIRECTION('center_axis',(0.,-0.707106781186546,-0.707106781186549));
#18774=DIRECTION('ref_axis',(-1.,0.,0.));
#18775=DIRECTION('',(0.,-0.707106781186549,0.707106781186546));
#18776=DIRECTION('',(1.,0.,0.));
#18777=DIRECTION('center_axis',(0.577350269189627,-0.577350269189624,-0.577350269189627));
#18778=DIRECTION('ref_axis',(-0.707106781186548,0.,-0.707106781186548));
#18779=DIRECTION('',(0.812519920068745,0.336556770590783,0.475963149477964));
#18780=DIRECTION('',(0.475963149477959,-0.336556770590788,0.812519920068746));
#18781=DIRECTION('',(-0.707106781186548,0.,-0.707106781186548));
#18782=DIRECTION('center_axis',(2.16784530188846E-15,-1.,0.));
#18783=DIRECTION('ref_axis',(-1.,0.,0.));
#18784=DIRECTION('center_axis',(0.,1.,0.));
#18785=DIRECTION('ref_axis',(-1.,0.,0.));
#18786=DIRECTION('center_axis',(0.,1.,0.));
#18787=DIRECTION('ref_axis',(-1.,0.,0.));
#18788=DIRECTION('',(0.38268343236509,-0.923879532511287,-4.68652040532627E-17));
#18789=DIRECTION('center_axis',(0.,-1.,-3.96079183235886E-16));
#18790=DIRECTION('ref_axis',(-1.,0.,0.));
#18791=DIRECTION('center_axis',(0.,-1.,-3.96079183235886E-16));
#18792=DIRECTION('ref_axis',(-1.,0.,0.));
#18793=DIRECTION('center_axis',(0.,-1.,0.));
#18794=DIRECTION('ref_axis',(1.,0.,0.));
#18795=DIRECTION('center_axis',(0.,-1.,0.));
#18796=DIRECTION('ref_axis',(-1.,0.,0.));
#18797=DIRECTION('center_axis',(0.,-1.,0.));
#18798=DIRECTION('ref_axis',(-1.,0.,0.));
#18799=DIRECTION('',(0.,-1.,0.));
#18800=DIRECTION('center_axis',(0.,-1.,0.));
#18801=DIRECTION('ref_axis',(1.,0.,0.));
#18802=DIRECTION('',(-0.707106781186548,-0.707106781186548,-8.65956056235493E-17));
#18803=DIRECTION('center_axis',(-9.83554226541497E-17,1.,3.93421690616599E-16));
#18804=DIRECTION('ref_axis',(1.,9.83554226541497E-17,0.));
#18805=DIRECTION('center_axis',(0.,1.,0.));
#18806=DIRECTION('ref_axis',(-1.,0.,0.));
#18807=DIRECTION('center_axis',(0.,1.,0.));
#18808=DIRECTION('ref_axis',(-1.,0.,0.));
#18809=DIRECTION('',(-0.707106781186548,-0.707106781186548,8.65956056235493E-17));
#18810=DIRECTION('center_axis',(0.,-1.,0.));
#18811=DIRECTION('ref_axis',(0.,0.,-1.));
#18812=DIRECTION('center_axis',(0.,-1.,0.));
#18813=DIRECTION('ref_axis',(1.,0.,0.));
#18814=DIRECTION('center_axis',(0.,1.,0.));
#18815=DIRECTION('ref_axis',(-1.,0.,0.));
#18816=DIRECTION('center_axis',(0.,1.,0.));
#18817=DIRECTION('ref_axis',(-1.,0.,0.));
#18818=DIRECTION('',(-0.707106781186547,-0.707106781186547,8.65956056235493E-17));
#18819=DIRECTION('center_axis',(0.,-1.,0.));
#18820=DIRECTION('ref_axis',(-1.,0.,0.));
#18821=DIRECTION('center_axis',(0.,-1.,0.));
#18822=DIRECTION('ref_axis',(-1.,0.,0.));
#18823=DIRECTION('center_axis',(0.,-1.,0.));
#18824=DIRECTION('ref_axis',(0.,0.,-1.));
#18825=DIRECTION('center_axis',(0.,-1.,0.));
#18826=DIRECTION('ref_axis',(1.,0.,0.));
#18827=DIRECTION('center_axis',(0.,-1.,0.));
#18828=DIRECTION('ref_axis',(1.,0.,0.));
#18829=DIRECTION('',(0.,-1.,0.));
#18830=DIRECTION('center_axis',(0.,1.,0.));
#18831=DIRECTION('ref_axis',(1.,0.,0.));
#18832=DIRECTION('',(0.707106781186548,-0.707106781186547,-8.65956056235494E-17));
#18833=DIRECTION('center_axis',(0.,-1.,0.));
#18834=DIRECTION('ref_axis',(1.,0.,0.));
#18835=DIRECTION('center_axis',(0.,-1.,0.));
#18836=DIRECTION('ref_axis',(1.,0.,0.));
#18837=DIRECTION('',(0.,-1.,0.));
#18838=DIRECTION('center_axis',(0.,1.,0.));
#18839=DIRECTION('ref_axis',(0.,0.,1.));
#18840=DIRECTION('',(8.65956056235484E-17,-0.707106781186555,0.70710678118654));
#18841=DIRECTION('center_axis',(0.,-1.,0.));
#18842=DIRECTION('ref_axis',(0.,0.,1.));
#18843=DIRECTION('center_axis',(0.,1.,0.));
#18844=DIRECTION('ref_axis',(0.,0.,1.));
#18845=DIRECTION('center_axis',(0.,1.,0.));
#18846=DIRECTION('ref_axis',(0.,0.,-1.));
#18847=DIRECTION('center_axis',(0.,1.,0.));
#18848=DIRECTION('ref_axis',(0.,0.,-1.));
#18849=DIRECTION('',(0.,1.,0.));
#18850=DIRECTION('center_axis',(0.,-1.,0.));
#18851=DIRECTION('ref_axis',(0.,0.,-1.));
#18852=DIRECTION('center_axis',(0.,-1.,0.));
#18853=DIRECTION('ref_axis',(0.,0.,-1.));
#18854=DIRECTION('',(8.65956056235484E-17,0.707106781186555,-0.70710678118654));
#18855=DIRECTION('center_axis',(0.,1.,0.));
#18856=DIRECTION('ref_axis',(0.,0.,1.));
#18857=DIRECTION('center_axis',(0.,1.,0.));
#18858=DIRECTION('ref_axis',(1.,0.,0.));
#18859=DIRECTION('center_axis',(0.,1.,0.));
#18860=DIRECTION('ref_axis',(0.,0.,1.));
#18861=DIRECTION('',(8.65956056235497E-17,-0.707106781186545,0.70710678118655));
#18862=DIRECTION('center_axis',(0.,-1.,0.));
#18863=DIRECTION('ref_axis',(0.,0.,1.));
#18864=DIRECTION('center_axis',(0.,1.,0.));
#18865=DIRECTION('ref_axis',(0.,0.,1.));
#18866=DIRECTION('center_axis',(0.,1.,0.));
#18867=DIRECTION('ref_axis',(0.,0.,-1.));
#18868=DIRECTION('center_axis',(0.,1.,0.));
#18869=DIRECTION('ref_axis',(0.,0.,-1.));
#18870=DIRECTION('',(0.,1.,0.));
#18871=DIRECTION('center_axis',(0.,-1.,0.));
#18872=DIRECTION('ref_axis',(0.,0.,-1.));
#18873=DIRECTION('center_axis',(0.,-1.,0.));
#18874=DIRECTION('ref_axis',(0.,0.,-1.));
#18875=DIRECTION('',(8.65956056235497E-17,0.707106781186545,-0.70710678118655));
#18876=DIRECTION('center_axis',(0.,1.,0.));
#18877=DIRECTION('ref_axis',(0.,0.,1.));
#18878=DIRECTION('center_axis',(0.,1.,0.));
#18879=DIRECTION('ref_axis',(1.,0.,0.));
#18880=DIRECTION('center_axis',(0.,1.,0.));
#18881=DIRECTION('ref_axis',(0.,0.,1.));
#18882=DIRECTION('',(8.65956056235496E-17,-0.707106781186545,0.70710678118655));
#18883=DIRECTION('center_axis',(0.,-1.,0.));
#18884=DIRECTION('ref_axis',(0.,0.,1.));
#18885=DIRECTION('center_axis',(0.,1.,0.));
#18886=DIRECTION('ref_axis',(0.,0.,1.));
#18887=DIRECTION('center_axis',(0.,1.,0.));
#18888=DIRECTION('ref_axis',(0.,0.,1.));
#18889=DIRECTION('',(0.,1.,0.));
#18890=DIRECTION('center_axis',(0.,1.,0.));
#18891=DIRECTION('ref_axis',(0.,0.,1.));
#18892=DIRECTION('',(8.65956056235484E-17,-0.707106781186555,0.70710678118654));
#18893=DIRECTION('center_axis',(0.,-1.,0.));
#18894=DIRECTION('ref_axis',(0.,0.,1.));
#18895=DIRECTION('center_axis',(0.,1.,0.));
#18896=DIRECTION('ref_axis',(0.,0.,1.));
#18897=DIRECTION('center_axis',(0.,1.,0.));
#18898=DIRECTION('ref_axis',(0.,0.,1.));
#18899=DIRECTION('',(0.,1.,0.));
#18900=DIRECTION('center_axis',(0.,1.,0.));
#18901=DIRECTION('ref_axis',(0.,0.,1.));
#18902=DIRECTION('',(8.65956056235496E-17,-0.707106781186545,0.70710678118655));
#18903=DIRECTION('center_axis',(0.,-1.,0.));
#18904=DIRECTION('ref_axis',(0.,0.,1.));
#18905=DIRECTION('center_axis',(0.,1.,0.));
#18906=DIRECTION('ref_axis',(0.,0.,1.));
#18907=DIRECTION('center_axis',(0.,1.,0.));
#18908=DIRECTION('ref_axis',(0.,0.,1.));
#18909=DIRECTION('',(0.,1.,0.));
#18910=DIRECTION('center_axis',(0.,-1.,0.));
#18911=DIRECTION('ref_axis',(0.,0.,1.));
#18912=DIRECTION('center_axis',(0.,-1.,0.));
#18913=DIRECTION('ref_axis',(0.,0.,1.));
#18914=DIRECTION('',(-8.65956056235496E-17,0.707106781186545,0.70710678118655));
#18915=DIRECTION('center_axis',(0.,1.,0.));
#18916=DIRECTION('ref_axis',(0.,0.,1.));
#18917=DIRECTION('center_axis',(0.,1.,0.));
#18918=DIRECTION('ref_axis',(1.,0.,0.));
#18919=DIRECTION('',(0.,0.,-1.));
#18920=DIRECTION('',(1.,0.,0.));
#18921=DIRECTION('',(0.,0.,1.));
#18922=DIRECTION('',(-1.,0.,0.));
#18923=DIRECTION('center_axis',(0.,-1.,0.));
#18924=DIRECTION('ref_axis',(0.,0.,1.));
#18925=DIRECTION('center_axis',(0.,-1.,0.));
#18926=DIRECTION('ref_axis',(0.,0.,1.));
#18927=DIRECTION('center_axis',(0.,-1.,0.));
#18928=DIRECTION('ref_axis',(0.,0.,1.));
#18929=DIRECTION('center_axis',(0.,-1.,0.));
#18930=DIRECTION('ref_axis',(0.,0.,1.));
#18931=DIRECTION('center_axis',(0.,-1.,0.));
#18932=DIRECTION('ref_axis',(1.,0.,0.));
#18933=DIRECTION('center_axis',(0.,1.,0.));
#18934=DIRECTION('ref_axis',(0.,0.,1.));
#18935=DIRECTION('',(0.,1.,0.));
#18936=DIRECTION('center_axis',(0.,-1.,0.));
#18937=DIRECTION('ref_axis',(0.,0.,1.));
#18938=DIRECTION('',(-8.65956056235484E-17,0.707106781186555,0.70710678118654));
#18939=DIRECTION('center_axis',(0.,1.,0.));
#18940=DIRECTION('ref_axis',(0.,0.,1.));
#18941=DIRECTION('center_axis',(0.,1.,0.));
#18942=DIRECTION('ref_axis',(0.,0.,1.));
#18943=DIRECTION('',(0.,1.,0.));
#18944=DIRECTION('center_axis',(0.,-1.,0.));
#18945=DIRECTION('ref_axis',(1.,4.80868578370782E-17,0.));
#18946=DIRECTION('',(0.923879532511286,0.382683432365092,1.1314261122877E-16));
#18947=DIRECTION('center_axis',(0.382683432365095,-0.923879532511285,0.));
#18948=DIRECTION('ref_axis',(0.,0.,-1.));
#18949=DIRECTION('',(-0.678598344545843,-0.281084637714823,-0.67859834454585));
#18950=DIRECTION('',(0.678598344545851,0.281084637714827,-0.678598344545841));
#18951=DIRECTION('center_axis',(0.,-0.923879532511286,0.382683432365092));
#18952=DIRECTION('ref_axis',(0.,-0.382683432365092,-0.923879532511286));
#18953=DIRECTION('',(-0.678598344545843,0.281084637714823,0.67859834454585));
#18954=DIRECTION('center_axis',(-0.382683432365095,-0.923879532511285,0.));
#18955=DIRECTION('ref_axis',(0.,0.,-1.));
#18956=DIRECTION('',(0.678598344545851,-0.281084637714827,0.678598344545841));
#18957=DIRECTION('center_axis',(0.,-0.923879532511283,-0.3826834323651));
#18958=DIRECTION('ref_axis',(0.,0.3826834323651,-0.923879532511283));
#18959=DIRECTION('center_axis',(0.,-1.,0.));
#18960=DIRECTION('ref_axis',(0.,0.,1.));
#18961=DIRECTION('',(-8.65956056235496E-17,0.707106781186545,0.70710678118655));
#18962=DIRECTION('center_axis',(0.,-1.,0.));
#18963=DIRECTION('ref_axis',(0.,0.,1.));
#18964=DIRECTION('',(-8.65956056235484E-17,0.707106781186555,0.70710678118654));
#18965=DIRECTION('center_axis',(0.,-1.,0.));
#18966=DIRECTION('ref_axis',(0.,0.,1.));
#18967=DIRECTION('',(-8.65956056235496E-17,0.707106781186545,0.70710678118655));
#18968=DIRECTION('center_axis',(-0.707106781186554,0.,-0.707106781186541));
#18969=DIRECTION('ref_axis',(-0.707106781186541,0.,0.707106781186554));
#18970=DIRECTION('center_axis',(0.707106781186554,0.,0.707106781186541));
#18971=DIRECTION('ref_axis',(0.707106781186541,0.,-0.707106781186554));
#18972=DIRECTION('center_axis',(0.707106781186548,0.,-0.707106781186548));
#18973=DIRECTION('ref_axis',(-0.707106781186548,0.,-0.707106781186548));
#22961=CARTESIAN_POINT('',(0.,0.,0.));
#22962=CARTESIAN_POINT('Origin',(2.7893933982822,-0.104393398282202,11.3));
#22963=CARTESIAN_POINT('',(2.78432776750217,-0.0921638837510863,6.44216388375109));
#22964=CARTESIAN_POINT('',(2.7787867965644,-0.0787867965644036,6.45));
#22965=CARTESIAN_POINT('',(2.39970611825836,0.836394918235631,6.98610103649399));
#22966=CARTESIAN_POINT('',(2.7787867965644,-0.0787867965644036,11.95));
#22967=CARTESIAN_POINT('',(2.7787867965644,-0.0787867965644035,11.3));
#22968=CARTESIAN_POINT('',(2.78432776750218,-0.092163883751089,11.9578361162489));
#22969=CARTESIAN_POINT('',(2.7349292673093,0.0270946453754314,11.8879760873153));
#22970=CARTESIAN_POINT('',(2.8,-0.13,11.92));
#22971=CARTESIAN_POINT('',(2.92207588469155,-0.424717256461034,11.625282743539));
#22972=CARTESIAN_POINT('',(2.8,-0.13,6.48));
#22973=CARTESIAN_POINT('',(2.8,-0.13,11.3));
#22974=CARTESIAN_POINT('',(3.32263738133569,-1.3917582542238,7.74175825422382));
#22975=CARTESIAN_POINT('Origin',(2.7893933982822,-0.85,11.9456066017178));
#22976=CARTESIAN_POINT('',(2.7787867965644,-0.1,11.9712132034356));
#22977=CARTESIAN_POINT('',(2.72691983628388,-0.173350958667782,12.0964311223839));
#22978=CARTESIAN_POINT('',(2.7787867965644,-0.8,11.9712132034356));
#22979=CARTESIAN_POINT('',(2.7787867965644,-0.85,11.9712132034356));
#22980=CARTESIAN_POINT('',(2.78757359312881,-0.812426406871192,11.95));
#22981=CARTESIAN_POINT('',(2.79216823850424,-0.818924216675421,11.9389075448203));
#22982=CARTESIAN_POINT('',(2.8,-0.8,11.92));
#22983=CARTESIAN_POINT('',(2.99252497643701,-0.607475023562985,11.4552035907902));
#22984=CARTESIAN_POINT('',(2.8,-0.85,11.92));
#22985=CARTESIAN_POINT('Origin',(2.8,-0.1,11.95));
#22986=CARTESIAN_POINT('',(2.7712132034356,-0.0712132034355967,11.95));
#22987=CARTESIAN_POINT('',(2.75,-0.0499999999999999,11.95));
#22988=CARTESIAN_POINT('',(2.75783611624891,-0.0656722324978244,11.9578361162489));
#22989=CARTESIAN_POINT('',(3.17114651601527,-0.2368710055509,11.7157244895356));
#22990=CARTESIAN_POINT('',(2.75,-0.0712132034355964,11.9712132034356));
#22991=CARTESIAN_POINT('',(2.37247760726871,-0.338161847385669,12.615684240117));
#22992=CARTESIAN_POINT('',(2.75,-0.0787867965644033,11.9787867965644));
#22993=CARTESIAN_POINT('',(2.75,-0.1,12.));
#22994=CARTESIAN_POINT('',(2.75783611624891,-0.0921638837510902,11.9843277675022));
#22995=CARTESIAN_POINT('',(2.21389896350601,0.836394918235626,11.5997061182584));
#22996=CARTESIAN_POINT('',(2.77121320343559,-0.1,11.9787867965644));
#22997=CARTESIAN_POINT('',(2.9197723149051,-0.187023912684747,11.9172515977796));
#22998=CARTESIAN_POINT('',(2.8,-0.1,11.95));
#22999=CARTESIAN_POINT('Origin',(2.775,-0.075,10.6));
#23000=CARTESIAN_POINT('',(2.7712132034356,-0.0712132034355967,6.45));
#23001=CARTESIAN_POINT('',(2.8,-0.1,6.45));
#23002=CARTESIAN_POINT('',(2.7712132034356,-0.0712132034355966,9.9));
#23003=CARTESIAN_POINT('Origin',(2.7893933982822,-0.85,6.4543933982822));
#23004=CARTESIAN_POINT('',(2.8,-0.8,6.48));
#23005=CARTESIAN_POINT('',(2.8,-0.85,6.48));
#23006=CARTESIAN_POINT('',(2.78757359312881,-0.812426406871193,6.45));
#23007=CARTESIAN_POINT('',(3.42427185655271,-0.175728143447283,7.98712558269742));
#23008=CARTESIAN_POINT('',(2.7787867965644,-0.8,6.4287867965644));
#23009=CARTESIAN_POINT('',(2.79216823850424,-0.818924216675423,6.46109245517966));
#23010=CARTESIAN_POINT('',(2.7787867965644,-0.1,6.4287867965644));
#23011=CARTESIAN_POINT('',(2.7787867965644,-0.85,6.4287867965644));
#23012=CARTESIAN_POINT('',(2.71725159777964,-0.187023912684737,6.2802276850949));
#23013=CARTESIAN_POINT('Origin',(2.8,-0.85,12.));
#23014=CARTESIAN_POINT('',(2.8,-0.8,10.6));
#23015=CARTESIAN_POINT('Origin',(2.75,-0.1,6.4));
#23016=CARTESIAN_POINT('',(2.7712132034356,-0.1,6.4212132034356));
#23017=CARTESIAN_POINT('',(2.75,-0.1,6.4));
#23018=CARTESIAN_POINT('',(2.75783611624891,-0.092163883751087,6.41567223249783));
#23019=CARTESIAN_POINT('',(2.8964311223839,-0.173350958667782,6.47308016371612));
#23020=CARTESIAN_POINT('',(2.75,-0.0787867965644033,6.4212132034356));
#23021=CARTESIAN_POINT('',(2.68797608731527,0.0270946453754293,6.4650707326907));
#23022=CARTESIAN_POINT('',(2.75,-0.0712132034355962,6.4287867965644));
#23023=CARTESIAN_POINT('',(2.75,-0.0499999999999999,6.45));
#23024=CARTESIAN_POINT('',(2.75783611624891,-0.0656722324978246,6.44216388375109));
#23025=CARTESIAN_POINT('',(2.51572448953563,-0.236871005550898,6.02885348398473));
#23026=CARTESIAN_POINT('',(3.41568424011697,-0.338161847385675,6.8275223927313));
#23027=CARTESIAN_POINT('Origin',(2.775,-0.825,10.6));
#23028=CARTESIAN_POINT('',(2.7712132034356,-0.828786796564403,11.95));
#23029=CARTESIAN_POINT('',(2.8,-0.8,11.95));
#23030=CARTESIAN_POINT('',(2.7712132034356,-0.828786796564403,6.45));
#23031=CARTESIAN_POINT('',(2.7712132034356,-0.828786796564403,9.9));
#23032=CARTESIAN_POINT('',(2.75,-0.85,6.45));
#23033=CARTESIAN_POINT('Origin',(2.75,-0.85,11.95));
#23034=CARTESIAN_POINT('',(2.77121320343559,-0.8,11.9787867965644));
#23035=CARTESIAN_POINT('',(2.75,-0.8,12.));
#23036=CARTESIAN_POINT('',(2.75783611624892,-0.80783611624891,11.9843277675022));
#23037=CARTESIAN_POINT('',(2.73890754482034,-0.818924216675422,11.9921682385042));
#23038=CARTESIAN_POINT('',(2.75,-0.821213203435597,11.9787867965644));
#23039=CARTESIAN_POINT('',(2.19856720201026,-1.76256787225257,11.5888649257372));
#23040=CARTESIAN_POINT('',(2.75,-0.828786796564404,11.9712132034356));
#23041=CARTESIAN_POINT('',(2.75,-0.85,11.95));
#23042=CARTESIAN_POINT('',(2.75783611624891,-0.834327767502176,11.9578361162489));
#23043=CARTESIAN_POINT('',(2.3708187997899,-0.56066519859738,12.6185160016127));
#23044=CARTESIAN_POINT('',(3.14780532349409,-0.672797232953338,11.7293974435526));
#23045=CARTESIAN_POINT('Origin',(2.1,-0.104393398282202,6.4106066017178));
#23046=CARTESIAN_POINT('',(-2.75783611624891,-0.0921638837510879,6.41567223249783));
#23047=CARTESIAN_POINT('',(-2.75,-0.0787867965644033,6.4212132034356));
#23048=CARTESIAN_POINT('',(-2.21389896350603,0.836394918235614,6.80029388174163));
#23049=CARTESIAN_POINT('',(2.1,-0.0787867965644035,6.4212132034356));
#23050=CARTESIAN_POINT('',(2.72,-0.13,6.4));
#23051=CARTESIAN_POINT('',(2.42528274353897,-0.424717256461035,6.27792411530845));
#23052=CARTESIAN_POINT('',(-2.72,-0.13,6.4));
#23053=CARTESIAN_POINT('',(2.1,-0.13,6.4));
#23054=CARTESIAN_POINT('',(-1.45824174577622,-1.3917582542238,5.8773626186643));
#23055=CARTESIAN_POINT('Origin',(-2.7456066017178,-0.85,6.4106066017178));
#23056=CARTESIAN_POINT('',(-2.72,-0.769999999999999,6.4));
#23057=CARTESIAN_POINT('',(-2.72,-0.85,6.4));
#23058=CARTESIAN_POINT('',(-2.75783611624891,-0.807836116248913,6.41567223249782));
#23059=CARTESIAN_POINT('',(-1.64244003106437,0.30755996893565,5.95366004659652));
#23060=CARTESIAN_POINT('',(-2.7712132034356,-0.8,6.4212132034356));
#23061=CARTESIAN_POINT('',(-2.73890754482034,-0.818924216675422,6.40783176149576));
#23062=CARTESIAN_POINT('',(-2.7712132034356,-0.1,6.4212132034356));
#23063=CARTESIAN_POINT('',(-2.7712132034356,-0.85,6.4212132034356));
#23064=CARTESIAN_POINT('',(-2.9197723149051,-0.187023912684738,6.48274840222036));
#23065=CARTESIAN_POINT('Origin',(2.8,-0.85,6.4));
#23066=CARTESIAN_POINT('',(2.72,-0.769999999999999,6.4));
#23067=CARTESIAN_POINT('',(2.72,-0.85,6.4));
#23068=CARTESIAN_POINT('',(2.1,-0.769999999999999,6.4));
#23069=CARTESIAN_POINT('Origin',(2.7456066017178,-0.85,6.4106066017178));
#23070=CARTESIAN_POINT('',(2.7712132034356,-0.8,6.4212132034356));
#23071=CARTESIAN_POINT('',(2.7712132034356,-0.85,6.4212132034356));
#23072=CARTESIAN_POINT('',(2.75783611624891,-0.807836116248912,6.41567223249782));
#23073=CARTESIAN_POINT('',(2.73890754482034,-0.818924216675421,6.40783176149576));
#23074=CARTESIAN_POINT('',(2.60948102882711,-0.659481028827113,6.35422154324067));
#23075=CARTESIAN_POINT('Origin',(1.4,-0.075,6.425));
#23076=CARTESIAN_POINT('',(-2.75,-0.0712132034355962,6.4287867965644));
#23077=CARTESIAN_POINT('',(-2.75,-0.1,6.4));
#23078=CARTESIAN_POINT('',(0.7,-0.0712132034355964,6.4287867965644));
#23079=CARTESIAN_POINT('Origin',(-2.8,-0.1,6.45));
#23080=CARTESIAN_POINT('',(-2.7787867965644,-0.1,6.4287867965644));
#23081=CARTESIAN_POINT('',(-2.8,-0.1,6.45));
#23082=CARTESIAN_POINT('',(-2.78432776750217,-0.0921638837510875,6.44216388375109));
#23083=CARTESIAN_POINT('',(-2.72691983628388,-0.173350958667781,6.3035688776161));
#23084=CARTESIAN_POINT('',(-2.7787867965644,-0.0787867965644036,6.45));
#23085=CARTESIAN_POINT('',(-2.73492926730931,0.0270946453754293,6.51202391268473));
#23086=CARTESIAN_POINT('',(-2.7712132034356,-0.0712132034355967,6.45));
#23087=CARTESIAN_POINT('',(-2.75,-0.0499999999999999,6.45));
#23088=CARTESIAN_POINT('',(-2.75783611624891,-0.0656722324978246,6.44216388375109));
#23089=CARTESIAN_POINT('',(-3.17114651601528,-0.236871005550901,6.68427551046438));
#23090=CARTESIAN_POINT('',(-2.37247760726871,-0.338161847385672,5.78431575988303));
#23091=CARTESIAN_POINT('Origin',(-2.7893933982822,-0.104393398282202,7.1));
#23092=CARTESIAN_POINT('',(-2.78432776750218,-0.0921638837510882,11.9578361162489));
#23093=CARTESIAN_POINT('',(-2.7787867965644,-0.0787867965644036,11.95));
#23094=CARTESIAN_POINT('',(-2.39970611825836,0.836394918235639,11.413898963506));
#23095=CARTESIAN_POINT('',(-2.7787867965644,-0.0787867965644035,7.1));
#23096=CARTESIAN_POINT('',(-2.8,-0.13,6.48));
#23097=CARTESIAN_POINT('',(-2.92207588469155,-0.424717256461036,6.77471725646103));
#23098=CARTESIAN_POINT('',(-2.8,-0.13,11.92));
#23099=CARTESIAN_POINT('',(-2.8,-0.13,7.1));
#23100=CARTESIAN_POINT('',(-3.3226373813357,-1.3917582542238,10.6582417457763));
#23101=CARTESIAN_POINT('Origin',(-2.7893933982822,-0.85,11.9456066017178));
#23102=CARTESIAN_POINT('',(-2.8,-0.8,11.92));
#23103=CARTESIAN_POINT('',(-2.8,-0.85,11.92));
#23104=CARTESIAN_POINT('',(-2.78757359312881,-0.812426406871193,11.95));
#23105=CARTESIAN_POINT('',(-3.42427185655274,-0.175728143447254,10.4128744173027));
#23106=CARTESIAN_POINT('',(-2.7787867965644,-0.8,11.9712132034356));
#23107=CARTESIAN_POINT('',(-2.78132704598305,-0.803592455179658,11.9650804988373));
#23108=CARTESIAN_POINT('',(-2.7787867965644,-0.1,11.9712132034356));
#23109=CARTESIAN_POINT('',(-2.7787867965644,-0.85,11.9712132034356));
#23110=CARTESIAN_POINT('',(-2.71725159777964,-0.187023912684724,12.1197723149051));
#23111=CARTESIAN_POINT('Origin',(-2.8,-0.85,6.4));
#23112=CARTESIAN_POINT('',(-2.8,-0.8,6.48));
#23113=CARTESIAN_POINT('',(-2.8,-0.85,6.48));
#23114=CARTESIAN_POINT('',(-2.8,-0.8,7.8));
#23115=CARTESIAN_POINT('Origin',(-2.7893933982822,-0.85,6.4543933982822));
#23116=CARTESIAN_POINT('',(-2.7787867965644,-0.8,6.4287867965644));
#23117=CARTESIAN_POINT('',(-2.7787867965644,-0.85,6.4287867965644));
#23118=CARTESIAN_POINT('',(-2.78757359312881,-0.812426406871193,6.45));
#23119=CARTESIAN_POINT('',(-2.79216823850424,-0.818924216675421,6.46109245517966));
#23120=CARTESIAN_POINT('',(-2.99252497643702,-0.607475023562983,6.9447964092098));
#23121=CARTESIAN_POINT('Origin',(-2.775,-0.825,7.8));
#23122=CARTESIAN_POINT('',(-2.7712132034356,-0.828786796564403,6.45));
#23123=CARTESIAN_POINT('',(-2.8,-0.8,6.45));
#23124=CARTESIAN_POINT('',(-2.7712132034356,-0.828786796564403,11.95));
#23125=CARTESIAN_POINT('',(-2.7712132034356,-0.828786796564403,8.5));
#23126=CARTESIAN_POINT('',(-2.75,-0.85,11.95));
#23127=CARTESIAN_POINT('Origin',(-2.75,-0.85,6.45));
#23128=CARTESIAN_POINT('',(-2.75,-0.821213203435597,6.4212132034356));
#23129=CARTESIAN_POINT('',(-2.19856720201027,-1.76256787225257,6.81113507426282));
#23130=CARTESIAN_POINT('',(-2.75,-0.828786796564403,6.4287867965644));
#23131=CARTESIAN_POINT('',(-2.75,-0.85,6.45));
#23132=CARTESIAN_POINT('',(-2.75783611624891,-0.834327767502175,6.44216388375109));
#23133=CARTESIAN_POINT('',(-2.37081879978991,-0.560665198597375,5.78148399838728));
#23134=CARTESIAN_POINT('',(-3.14780532349409,-0.672797232953337,6.67060255644743));
#23135=CARTESIAN_POINT('',(-2.75,-0.8,6.4));
#23136=CARTESIAN_POINT('Origin',(-2.75,-0.1,12.));
#23137=CARTESIAN_POINT('',(-2.77121320343559,-0.1,11.9787867965644));
#23138=CARTESIAN_POINT('',(-2.75,-0.1,12.));
#23139=CARTESIAN_POINT('',(-2.75783611624891,-0.0921638837510905,11.9843277675022));
#23140=CARTESIAN_POINT('',(-2.89643112238391,-0.173350958667796,11.9269198362839));
#23141=CARTESIAN_POINT('',(-2.75,-0.0787867965644033,11.9787867965644));
#23142=CARTESIAN_POINT('',(-2.68797608731526,0.027094645375429,11.9349292673093));
#23143=CARTESIAN_POINT('',(-2.75,-0.0712132034355964,11.9712132034356));
#23144=CARTESIAN_POINT('',(-2.75,-0.0499999999999999,11.95));
#23145=CARTESIAN_POINT('',(-2.75783611624891,-0.0656722324978241,11.9578361162489));
#23146=CARTESIAN_POINT('',(-2.51572448953563,-0.236871005550895,12.3711465160153));
#23147=CARTESIAN_POINT('',(-2.7712132034356,-0.0712132034355967,11.95));
#23148=CARTESIAN_POINT('',(-3.41568424011698,-0.338161847385678,11.5724776072687));
#23149=CARTESIAN_POINT('',(-2.8,-0.1,11.95));
#23150=CARTESIAN_POINT('Origin',(-2.775,-0.85,11.975));
#23151=CARTESIAN_POINT('',(-2.77121320343559,-0.8,11.9787867965644));
#23152=CARTESIAN_POINT('',(-2.8,-0.8,11.95));
#23153=CARTESIAN_POINT('',(-2.7712132034356,-0.85,11.9787867965644));
#23154=CARTESIAN_POINT('Origin',(-2.75,-0.8,12.));
#23155=CARTESIAN_POINT('',(-2.75783611624891,-0.834327767502176,11.9578361162489));
#23156=CARTESIAN_POINT('',(-3.41568424011698,-0.561838152614322,11.5724776072687));
#23157=CARTESIAN_POINT('',(-2.75,-0.828786796564404,11.9712132034356));
#23158=CARTESIAN_POINT('',(-2.51572448953563,-0.663128994449105,12.3711465160153));
#23159=CARTESIAN_POINT('',(-2.75,-0.821213203435597,11.9787867965644));
#23160=CARTESIAN_POINT('',(-2.75,-0.8,12.));
#23161=CARTESIAN_POINT('',(-2.75783611624891,-0.80783611624891,11.9843277675022));
#23162=CARTESIAN_POINT('',(-2.68797608731526,-0.927094645375429,11.9349292673093));
#23163=CARTESIAN_POINT('',(-2.7417393063161,-0.817265409196609,11.9909952844873));
#23164=CARTESIAN_POINT('Origin',(-2.1,-0.104393398282201,11.9893933982822));
#23165=CARTESIAN_POINT('',(-2.1,-0.0787867965644031,11.9787867965644));
#23166=CARTESIAN_POINT('',(-2.72,-0.129999999999999,12.));
#23167=CARTESIAN_POINT('',(-2.42528274353895,-0.42471725646102,12.1220758846915));
#23168=CARTESIAN_POINT('',(2.72,-0.129999999999999,12.));
#23169=CARTESIAN_POINT('',(-2.1,-0.129999999999999,12.));
#23170=CARTESIAN_POINT('',(1.4582417457761,-1.39175825422379,12.5226373813357));
#23171=CARTESIAN_POINT('Origin',(-2.7456066017178,-0.85,11.9893933982822));
#23172=CARTESIAN_POINT('',(-2.72,-0.770000000000001,12.));
#23173=CARTESIAN_POINT('',(-2.6094810288271,-0.659481028827109,12.0457784567593));
#23174=CARTESIAN_POINT('',(-2.72,-0.85,12.));
#23175=CARTESIAN_POINT('Origin',(-1.4,-0.075,11.975));
#23176=CARTESIAN_POINT('',(-0.7,-0.0712132034355963,11.9712132034356));
#23177=CARTESIAN_POINT('Origin',(2.7456066017178,-0.85,11.9893933982822));
#23178=CARTESIAN_POINT('',(2.72,-0.770000000000001,12.));
#23179=CARTESIAN_POINT('',(2.72,-0.85,12.));
#23180=CARTESIAN_POINT('',(1.64244003106424,0.307559968935658,12.4463399534035));
#23181=CARTESIAN_POINT('',(2.77121320343559,-0.85,11.9787867965644));
#23182=CARTESIAN_POINT('Origin',(-2.1,-0.795606601717799,11.9893933982822));
#23183=CARTESIAN_POINT('',(-2.1,-0.770000000000001,12.));
#23184=CARTESIAN_POINT('',(-2.1,-0.821213203435597,11.9787867965644));
#23185=CARTESIAN_POINT('Origin',(-2.8,-0.85,12.));
#23186=CARTESIAN_POINT('Origin',(-2.7456066017178,-0.0606066017177983,8.5));
#23187=CARTESIAN_POINT('',(-2.7712132034356,-0.0712132034355966,8.5));
#23188=CARTESIAN_POINT('',(-2.72,-0.0499999999999999,11.92));
#23189=CARTESIAN_POINT('',(-1.48126653143723,0.463100202844175,10.6812665314372));
#23190=CARTESIAN_POINT('',(-2.72,-0.0499999999999999,6.48));
#23191=CARTESIAN_POINT('',(-2.72,-0.0499999999999999,8.5));
#23192=CARTESIAN_POINT('',(-1.48126653143723,0.463100202844175,7.71873346856278));
#23193=CARTESIAN_POINT('Origin',(-0.7,-0.0606066017177981,11.9456066017178));
#23194=CARTESIAN_POINT('',(2.72,-0.0499999999999999,11.92));
#23195=CARTESIAN_POINT('',(1.48126653143723,0.463100202844174,10.6812665314372));
#23196=CARTESIAN_POINT('',(-0.7,-0.0499999999999999,11.92));
#23197=CARTESIAN_POINT('Origin',(-2.775,-0.075,7.8));
#23198=CARTESIAN_POINT('Origin',(2.7456066017178,-0.0606066017177983,9.9));
#23199=CARTESIAN_POINT('',(2.72,-0.0499999999999999,6.48));
#23200=CARTESIAN_POINT('',(1.48126653143723,0.463100202844176,7.71873346856278));
#23201=CARTESIAN_POINT('',(2.72,-0.0499999999999999,9.9));
#23202=CARTESIAN_POINT('Origin',(0.,-0.0499999999999999,9.2));
#23203=CARTESIAN_POINT('',(0.7,-0.0499999999999999,6.48));
#23204=CARTESIAN_POINT('',(1.7,-0.0499999999999999,9.745));
#23205=CARTESIAN_POINT('Origin',(1.7,-0.0499999999999999,10.));
#23206=CARTESIAN_POINT('',(-2.,-0.0499999999999999,7.015));
#23207=CARTESIAN_POINT('Origin',(-2.,-0.0499999999999999,7.3));
#23208=CARTESIAN_POINT('',(2.,-0.0499999999999999,7.015));
#23209=CARTESIAN_POINT('Origin',(2.,-0.0499999999999999,7.3));
#23210=CARTESIAN_POINT('',(2.,-0.0499999999999999,10.815));
#23211=CARTESIAN_POINT('Origin',(2.,-0.0499999999999999,11.1));
#23212=CARTESIAN_POINT('',(-3.12284933782576E-17,-0.0499999999999999,7.045));
#23213=CARTESIAN_POINT('Origin',(0.,-0.0499999999999999,7.3));
#23214=CARTESIAN_POINT('',(-1.785,-0.0499999999999999,9.7));
#23215=CARTESIAN_POINT('Origin',(-0.4,-0.0499999999999999,9.7));
#23216=CARTESIAN_POINT('Origin',(0.7,-0.0606066017177982,6.4543933982822));
#23217=CARTESIAN_POINT('Origin',(-1.4,-0.825,11.975));
#23218=CARTESIAN_POINT('',(-0.7,-0.828786796564404,11.9712132034356));
#23219=CARTESIAN_POINT('Origin',(2.1,-0.795606601717798,6.4106066017178));
#23220=CARTESIAN_POINT('',(2.75,-0.821213203435597,6.4212132034356));
#23221=CARTESIAN_POINT('',(2.67430313329832,-0.950435837896618,6.47473897119493));
#23222=CARTESIAN_POINT('',(2.1,-0.821213203435596,6.4212132034356));
#23223=CARTESIAN_POINT('Origin',(1.4,-0.825,6.425));
#23224=CARTESIAN_POINT('',(2.75,-0.828786796564403,6.4287867965644));
#23225=CARTESIAN_POINT('',(2.75,-0.8,6.4));
#23226=CARTESIAN_POINT('',(0.7,-0.828786796564403,6.4287867965644));
#23227=CARTESIAN_POINT('Origin',(2.75,-0.85,6.45));
#23228=CARTESIAN_POINT('',(2.75783611624891,-0.834327767502175,6.44216388375109));
#23229=CARTESIAN_POINT('',(3.41851600161273,-0.560665198597375,6.82918120021011));
#23230=CARTESIAN_POINT('',(2.52939744355258,-0.672797232953338,6.05219467650592));
#23231=CARTESIAN_POINT('',(2.8,-0.8,6.45));
#23232=CARTESIAN_POINT('Origin',(-0.4,-0.795606601717798,9.7));
#23233=CARTESIAN_POINT('',(0.7,-0.77,9.7));
#23234=CARTESIAN_POINT('',(-1.5,-0.77,9.7));
#23235=CARTESIAN_POINT('Origin',(-0.4,-0.77,9.7));
#23236=CARTESIAN_POINT('Origin',(-0.4,-0.77,9.7));
#23237=CARTESIAN_POINT('',(0.721213203435596,-0.821213203435596,9.7));
#23238=CARTESIAN_POINT('',(0.710606601717798,-0.795606601717798,9.7));
#23239=CARTESIAN_POINT('',(-1.5212132034356,-0.821213203435596,9.7));
#23240=CARTESIAN_POINT('Origin',(-0.4,-0.821213203435596,9.7));
#23241=CARTESIAN_POINT('Origin',(-0.4,-0.821213203435596,9.7));
#23242=CARTESIAN_POINT('Origin',(-0.4,-0.75,9.7));
#23243=CARTESIAN_POINT('',(0.7,-0.73,9.7));
#23244=CARTESIAN_POINT('',(-1.5,-0.73,9.7));
#23245=CARTESIAN_POINT('Origin',(-0.4,-0.73,9.7));
#23246=CARTESIAN_POINT('Origin',(-0.4,-0.73,9.7));
#23247=CARTESIAN_POINT('',(-1.5,-0.75,9.7));
#23248=CARTESIAN_POINT('Origin',(-0.4,-0.84,9.7));
#23249=CARTESIAN_POINT('',(-1.5287867965644,-0.828786796564404,9.7));
#23250=CARTESIAN_POINT('',(-1.54,-0.84,9.7));
#23251=CARTESIAN_POINT('Origin',(-0.4,-0.828786796564404,9.7));
#23252=CARTESIAN_POINT('Origin',(-0.4,-0.715,9.7));
#23253=CARTESIAN_POINT('',(0.73,-0.7,9.7));
#23254=CARTESIAN_POINT('Origin',(-0.4,-0.7,9.7));
#23255=CARTESIAN_POINT('',(0.715,-0.715,9.7));
#23256=CARTESIAN_POINT('Origin',(0.7,-0.7,9.7));
#23257=CARTESIAN_POINT('',(-1.66,-0.7,9.7));
#23258=CARTESIAN_POINT('Origin',(-0.4,-0.7,9.7));
#23259=CARTESIAN_POINT('Origin',(-0.4,-0.415,9.7));
#23260=CARTESIAN_POINT('',(0.89,-0.4,9.7));
#23261=CARTESIAN_POINT('Origin',(-0.4,-0.4,9.7));
#23262=CARTESIAN_POINT('',(0.86,-0.43,9.7));
#23263=CARTESIAN_POINT('',(0.875,-0.415,9.7));
#23264=CARTESIAN_POINT('',(-1.66,-0.43,9.7));
#23265=CARTESIAN_POINT('Origin',(-0.4,-0.43,9.7));
#23266=CARTESIAN_POINT('Origin',(-0.4,-0.43,9.7));
#23267=CARTESIAN_POINT('Origin',(0.86,-0.4,9.7));
#23268=CARTESIAN_POINT('',(-1.755,-0.4,9.7));
#23269=CARTESIAN_POINT('Origin',(-0.4,-0.4,9.7));
#23270=CARTESIAN_POINT('Origin',(-0.4,-0.55,9.7));
#23271=CARTESIAN_POINT('',(-1.66,-0.55,9.7));
#23272=CARTESIAN_POINT('Origin',(-0.4,-0.0649999999999999,9.7));
#23273=CARTESIAN_POINT('',(-1.755,-0.0799999999999999,9.7));
#23274=CARTESIAN_POINT('',(-1.77,-0.0649999999999999,9.7));
#23275=CARTESIAN_POINT('Origin',(-0.4,-0.0799999999999999,9.7));
#23276=CARTESIAN_POINT('Origin',(-0.4,-0.21,9.7));
#23277=CARTESIAN_POINT('',(-1.755,-0.21,9.7));
#23278=CARTESIAN_POINT('Origin',(1.7,-0.0649999999999999,10.));
#23279=CARTESIAN_POINT('',(1.7,-0.0799999999999999,9.775));
#23280=CARTESIAN_POINT('',(1.7,-0.0649999999999999,9.76));
#23281=CARTESIAN_POINT('Origin',(1.7,-0.0799999999999999,10.));
#23282=CARTESIAN_POINT('Origin',(1.7,-0.135,10.));
#23283=CARTESIAN_POINT('',(1.7,-0.22,10.225));
#23284=CARTESIAN_POINT('',(1.7,-0.22,9.775));
#23285=CARTESIAN_POINT('Origin',(1.7,-0.22,10.));
#23286=CARTESIAN_POINT('Origin',(1.7,-0.22,10.));
#23287=CARTESIAN_POINT('',(1.7,-0.135,9.775));
#23288=CARTESIAN_POINT('Origin',(1.7,-0.235,10.));
#23289=CARTESIAN_POINT('',(1.7,-0.25,10.255));
#23290=CARTESIAN_POINT('Origin',(1.7,-0.25,10.));
#23291=CARTESIAN_POINT('',(1.7,-0.235,10.24));
#23292=CARTESIAN_POINT('Origin',(1.7,-0.25,10.225));
#23293=CARTESIAN_POINT('',(1.7,-0.25,9.6));
#23294=CARTESIAN_POINT('Origin',(1.7,-0.25,10.));
#23295=CARTESIAN_POINT('Origin',(0.,-0.0649999999999999,7.3));
#23296=CARTESIAN_POINT('',(2.75545529808155E-17,-0.0799999999999999,7.075));
#23297=CARTESIAN_POINT('',(-2.93915231795366E-17,-0.0649999999999999,7.06));
#23298=CARTESIAN_POINT('Origin',(0.,-0.0799999999999999,7.3));
#23299=CARTESIAN_POINT('Origin',(0.,-0.135,7.3));
#23300=CARTESIAN_POINT('',(2.75545529808155E-17,-0.22,7.525));
#23301=CARTESIAN_POINT('',(-2.75545529808155E-17,-0.22,7.075));
#23302=CARTESIAN_POINT('Origin',(0.,-0.22,7.3));
#23303=CARTESIAN_POINT('Origin',(0.,-0.22,7.3));
#23304=CARTESIAN_POINT('',(-2.75545529808155E-17,-0.135,7.075));
#23305=CARTESIAN_POINT('Origin',(0.,-0.235,7.3));
#23306=CARTESIAN_POINT('',(-3.12284933782576E-17,-0.25,7.555));
#23307=CARTESIAN_POINT('Origin',(0.,-0.25,7.3));
#23308=CARTESIAN_POINT('',(-2.93915231795366E-17,-0.235,7.54));
#23309=CARTESIAN_POINT('Origin',(0.,-0.25,7.525));
#23310=CARTESIAN_POINT('',(-4.89858719658942E-17,-0.25,6.9));
#23311=CARTESIAN_POINT('Origin',(0.,-0.25,7.3));
#23312=CARTESIAN_POINT('Origin',(-2.,-0.0649999999999999,7.3));
#23313=CARTESIAN_POINT('',(-2.,-0.08,7.045));
#23314=CARTESIAN_POINT('',(-2.,-0.0649999999999999,7.03));
#23315=CARTESIAN_POINT('Origin',(-2.,-0.08,7.3));
#23316=CARTESIAN_POINT('Origin',(-2.,-0.45,7.3));
#23317=CARTESIAN_POINT('',(-2.,-0.82,7.045));
#23318=CARTESIAN_POINT('Origin',(-2.,-0.82,7.3));
#23319=CARTESIAN_POINT('',(-2.,-0.45,7.045));
#23320=CARTESIAN_POINT('Origin',(2.,-0.0649999999999999,11.1));
#23321=CARTESIAN_POINT('',(2.,-0.08,10.845));
#23322=CARTESIAN_POINT('',(2.,-0.0649999999999999,10.83));
#23323=CARTESIAN_POINT('Origin',(2.,-0.08,11.1));
#23324=CARTESIAN_POINT('Origin',(2.,-0.45,11.1));
#23325=CARTESIAN_POINT('',(2.,-0.82,10.845));
#23326=CARTESIAN_POINT('Origin',(2.,-0.82,11.1));
#23327=CARTESIAN_POINT('',(2.,-0.45,10.845));
#23328=CARTESIAN_POINT('Origin',(2.,-0.0649999999999999,7.3));
#23329=CARTESIAN_POINT('',(2.,-0.08,7.045));
#23330=CARTESIAN_POINT('',(2.,-0.0649999999999999,7.03));
#23331=CARTESIAN_POINT('Origin',(2.,-0.08,7.3));
#23332=CARTESIAN_POINT('Origin',(2.,-0.45,7.3));
#23333=CARTESIAN_POINT('',(2.,-0.82,7.045));
#23334=CARTESIAN_POINT('Origin',(2.,-0.82,7.3));
#23335=CARTESIAN_POINT('',(2.,-0.45,7.045));
#23336=CARTESIAN_POINT('Origin',(0.,-0.835,7.3));
#23337=CARTESIAN_POINT('',(5.26598123633363E-17,-0.85,6.87));
#23338=CARTESIAN_POINT('Origin',(0.,-0.85,7.3));
#23339=CARTESIAN_POINT('',(-4.89858719658942E-17,-0.82,6.9));
#23340=CARTESIAN_POINT('',(5.08228421646152E-17,-0.835,6.885));
#23341=CARTESIAN_POINT('Origin',(0.,-0.82,7.3));
#23342=CARTESIAN_POINT('Origin',(0.,-0.85,9.2));
#23343=CARTESIAN_POINT('',(2.72,-0.85,11.92));
#23344=CARTESIAN_POINT('',(2.72,-0.85,6.48));
#23345=CARTESIAN_POINT('',(2.72,-0.85,9.9));
#23346=CARTESIAN_POINT('',(-2.72,-0.85,11.92));
#23347=CARTESIAN_POINT('',(-0.7,-0.85,11.92));
#23348=CARTESIAN_POINT('',(-2.72,-0.85,6.48));
#23349=CARTESIAN_POINT('',(-2.72,-0.85,8.5));
#23350=CARTESIAN_POINT('',(0.7,-0.85,6.48));
#23351=CARTESIAN_POINT('',(1.7,-0.85,9.57));
#23352=CARTESIAN_POINT('Origin',(1.7,-0.85,10.));
#23353=CARTESIAN_POINT('',(2.,-0.85,7.015));
#23354=CARTESIAN_POINT('Origin',(2.,-0.85,7.3));
#23355=CARTESIAN_POINT('',(-2.,-0.85,7.015));
#23356=CARTESIAN_POINT('Origin',(-2.,-0.85,7.3));
#23357=CARTESIAN_POINT('',(2.,-0.85,10.815));
#23358=CARTESIAN_POINT('Origin',(2.,-0.85,11.1));
#23359=CARTESIAN_POINT('',(-1.58,-0.85,9.7));
#23360=CARTESIAN_POINT('Origin',(-0.4,-0.85,9.7));
#23361=CARTESIAN_POINT('Origin',(0.,-0.565,7.3));
#23362=CARTESIAN_POINT('',(-4.89858719658942E-17,-0.565,6.9));
#23363=CARTESIAN_POINT('Origin',(1.7,-0.835,10.));
#23364=CARTESIAN_POINT('',(1.7,-0.82,9.6));
#23365=CARTESIAN_POINT('',(1.7,-0.835,9.585));
#23366=CARTESIAN_POINT('Origin',(1.7,-0.82,10.));
#23367=CARTESIAN_POINT('Origin',(1.7,-0.565,10.));
#23368=CARTESIAN_POINT('',(1.7,-0.565,9.6));
#23369=CARTESIAN_POINT('Origin',(-0.4,-0.839393398282202,9.7));
#23370=CARTESIAN_POINT('',(-1.5543933982822,-0.839393398282202,9.7));
#23371=CARTESIAN_POINT('Origin',(2.7456066017178,-0.839393398282202,9.9));
#23372=CARTESIAN_POINT('',(1.48126653143723,-1.36310020284417,10.6812665314372));
#23373=CARTESIAN_POINT('',(1.48126653143722,-1.36310020284418,7.71873346856276));
#23374=CARTESIAN_POINT('Origin',(-0.7,-0.839393398282202,11.9456066017178));
#23375=CARTESIAN_POINT('',(-1.48126653143723,-1.36310020284417,10.6812665314372));
#23376=CARTESIAN_POINT('Origin',(-2.7456066017178,-0.839393398282202,8.5));
#23377=CARTESIAN_POINT('',(-1.48126653143721,-1.36310020284418,7.71873346856277));
#23378=CARTESIAN_POINT('Origin',(0.7,-0.839393398282201,6.4543933982822));
#23379=CARTESIAN_POINT('Origin',(2.,-0.835,7.3));
#23380=CARTESIAN_POINT('',(2.,-0.835,7.03));
#23381=CARTESIAN_POINT('Origin',(2.,-0.835,11.1));
#23382=CARTESIAN_POINT('',(2.,-0.835,10.83));
#23383=CARTESIAN_POINT('Origin',(-2.,-0.835,7.3));
#23384=CARTESIAN_POINT('',(-2.,-0.835,7.03));
#23385=CARTESIAN_POINT('Origin',(-2.775,-0.85,6.425));
#23386=CARTESIAN_POINT('Origin',(2.775,-0.85,11.975));
#23387=CARTESIAN_POINT('Origin',(2.775,-0.85,6.425));
#38584=UNCERTAINTY_MEASURE_WITH_UNIT(LENGTH_MEASURE(0.001),#38612,
'DISTANCE_ACCURACY_VALUE',
'Maximum model space distance between geometric entities at asserted c
onnectivities');
#38595=UNCERTAINTY_MEASURE_WITH_UNIT(LENGTH_MEASURE(0.001),#38612,
'DISTANCE_ACCURACY_VALUE',
'Maximum model space distance between geometric entities at asserted c
onnectivities');
#38600=(
GEOMETRIC_REPRESENTATION_CONTEXT(3)
GLOBAL_UNCERTAINTY_ASSIGNED_CONTEXT((#38584))
GLOBAL_UNIT_ASSIGNED_CONTEXT((#38612,#38614,#38615))
REPRESENTATION_CONTEXT('','3D')
);
#38611=(
GEOMETRIC_REPRESENTATION_CONTEXT(3)
GLOBAL_UNCERTAINTY_ASSIGNED_CONTEXT((#38595))
GLOBAL_UNIT_ASSIGNED_CONTEXT((#38612,#38614,#38615))
REPRESENTATION_CONTEXT('','3D')
);
#38612=(
LENGTH_UNIT()
NAMED_UNIT(*)
SI_UNIT(.CENTI.,.METRE.)
);
#38614=(
NAMED_UNIT(*)
PLANE_ANGLE_UNIT()
SI_UNIT($,.RADIAN.)
);
#38615=(
NAMED_UNIT(*)
SI_UNIT($,.STERADIAN.)
SOLID_ANGLE_UNIT()
);
#38620=SHAPE_DEFINITION_REPRESENTATION(#38635,#38671);
#38635=PRODUCT_DEFINITION_SHAPE('',$,#38687);
#38671=SHAPE_REPRESENTATION('',(#16649),#38600);
#38682=PRODUCT_DEFINITION_CONTEXT('part definition',#38729,'design');
#38687=PRODUCT_DEFINITION('2026-10-19-02-31-31-424',
'05_Adjustable_Mirror_Plate_56x56',#38702,#38682);
#38702=PRODUCT_DEFINITION_FORMATION('',$,#38735);
#38729=APPLICATION_CONTEXT(
'Core Data for Automotive Mechanical Design Process');
#38730=PRODUCT_CONTEXT('part definition',#38729,'mechanical');
#38735=PRODUCT('2026-10-19-02-31-31-424',
'05_Adjustable_Mirror_Plate_56x56',$,(#38730));
#38865=COLOUR_RGB('Sky Blue',0.24,0.69,0.87);
#38866=FILL_AREA_STYLE_COLOUR('',#38865);
#38867=FILL_AREA_STYLE('',(#38866));
#38868=SURFACE_STYLE_FILL_AREA(#38867);
#38869=SURFACE_SIDE_STYLE('',(#38868));
#38870=SURFACE_STYLE_USAGE(.BOTH.,#38869);
#38871=PRESENTATION_STYLE_ASSIGNMENT((#38870));
ENDSEC;
END-ISO-10303-21;
